ISO-10303-21;
HEADER;
/* Generated by software containing ST-Developer
 * from STEP Tools, Inc. (www.steptools.com) 
 */

FILE_DESCRIPTION(
/* description */ (''),
/* implementation_level */ '2;1');

FILE_NAME(
/* name */ 'Disc.step',
/* time_stamp */ '2026-10-23T22:28:14+06:00',
/* author */ (''),
/* organization */ (''),
/* preprocessor_version */ 'ST-DEVELOPER v20.2',
/* originating_system */ 'Autodesk Translation Framework v15.15.0.0',
/* authorisation */ '');

FILE_SCHEMA (('AUTOMOTIVE_DESIGN { 1 0 10303 214 3 1 1 }'));
ENDSEC;

DATA;
#10=MECHANICAL_DESIGN_GEOMETRIC_PRESENTATION_REPRESENTATION('',(#108),#6753);
#69=B_SPLINE_CURVE_WITH_KNOTS('',3,(#5893,#5894,#5895,#5896,#5897,#5898,
#5899,#5900,#5901,#5902,#5903,#5904,#5905,#5906,#5907,#5908,#5909,#5910,
#5911,#5912,#5913,#5914,#5915,#5916,#5917,#5918,#5919,#5920,#5921,#5922,
#5923,#5924,#5925,#5926),.UNSPECIFIED.,.T.,.F.,(4,2,2,2,2,2,2,2,2,2,2,2,
2,2,2,2,4),(0.,0.0282524850207717,0.0565049700415435,0.0847574548366443,
0.113009939631745,0.141262424426846,0.169514909221947,0.197767394242719,
0.22601987926349,0.254272364284262,0.282524849305034,0.310777334100135,
0.339029818895236,0.367282303690336,0.395534788485437,0.423787273506209,
0.452039758526981),.UNSPECIFIED.);
#82=SHAPE_REPRESENTATION_RELATIONSHIP('SRR','None',#6805,#95);
#95=ADVANCED_BREP_SHAPE_REPRESENTATION('',(#121),#6745);
#108=STYLED_ITEM('',(#6907),#121);
#121=MANIFOLD_SOLID_BREP('Disc',#3757);
#170=FACE_BOUND('',#728,.T.);
#171=FACE_BOUND('',#730,.T.);
#209=PLANE('',#4051);
#210=PLANE('',#4052);
#211=PLANE('',#4053);
#212=PLANE('',#4054);
#213=PLANE('',#4055);
#214=PLANE('',#4056);
#215=PLANE('',#4057);
#216=PLANE('',#4058);
#217=PLANE('',#4059);
#218=PLANE('',#4060);
#219=PLANE('',#4061);
#220=PLANE('',#4062);
#221=PLANE('',#4063);
#222=PLANE('',#4064);
#223=PLANE('',#4065);
#224=PLANE('',#4066);
#225=PLANE('',#4067);
#226=PLANE('',#4068);
#227=PLANE('',#4069);
#228=PLANE('',#4070);
#229=PLANE('',#4071);
#230=PLANE('',#4076);
#231=PLANE('',#4079);
#232=PLANE('',#4082);
#233=PLANE('',#4085);
#234=PLANE('',#4088);
#235=PLANE('',#4091);
#236=PLANE('',#4094);
#237=PLANE('',#4097);
#238=PLANE('',#4100);
#239=PLANE('',#4103);
#240=PLANE('',#4106);
#241=PLANE('',#4109);
#242=PLANE('',#4112);
#243=PLANE('',#4115);
#244=PLANE('',#4118);
#245=PLANE('',#4121);
#246=PLANE('',#4124);
#247=PLANE('',#4127);
#248=PLANE('',#4130);
#249=PLANE('',#4131);
#250=PLANE('',#4132);
#251=PLANE('',#4133);
#252=PLANE('',#4134);
#253=PLANE('',#4135);
#254=PLANE('',#4136);
#255=PLANE('',#4137);
#256=PLANE('',#4138);
#257=PLANE('',#4139);
#258=PLANE('',#4140);
#259=PLANE('',#4141);
#260=PLANE('',#4142);
#261=PLANE('',#4143);
#262=PLANE('',#4144);
#263=PLANE('',#4145);
#264=PLANE('',#4146);
#265=PLANE('',#4147);
#266=PLANE('',#4148);
#267=PLANE('',#4172);
#268=PLANE('',#4174);
#269=PLANE('',#4176);
#270=PLANE('',#4178);
#271=PLANE('',#4180);
#272=PLANE('',#4182);
#273=PLANE('',#4184);
#274=PLANE('',#4186);
#275=PLANE('',#4188);
#276=PLANE('',#4190);
#277=PLANE('',#4192);
#278=PLANE('',#4194);
#279=PLANE('',#4196);
#280=PLANE('',#4198);
#281=PLANE('',#4200);
#282=PLANE('',#4202);
#283=PLANE('',#4204);
#284=PLANE('',#4206);
#285=PLANE('',#4208);
#286=PLANE('',#4210);
#287=PLANE('',#4211);
#288=PLANE('',#4213);
#289=PLANE('',#4217);
#290=PLANE('',#4218);
#391=FACE_OUTER_BOUND('',#645,.T.);
#392=FACE_OUTER_BOUND('',#646,.T.);
#393=FACE_OUTER_BOUND('',#647,.T.);
#394=FACE_OUTER_BOUND('',#648,.T.);
#395=FACE_OUTER_BOUND('',#649,.T.);
#396=FACE_OUTER_BOUND('',#650,.T.);
#397=FACE_OUTER_BOUND('',#651,.T.);
#398=FACE_OUTER_BOUND('',#652,.T.);
#399=FACE_OUTER_BOUND('',#653,.T.);
#400=FACE_OUTER_BOUND('',#654,.T.);
#401=FACE_OUTER_BOUND('',#655,.T.);
#402=FACE_OUTER_BOUND('',#656,.T.);
#403=FACE_OUTER_BOUND('',#657,.T.);
#404=FACE_OUTER_BOUND('',#658,.T.);
#405=FACE_OUTER_BOUND('',#659,.T.);
#406=FACE_OUTER_BOUND('',#660,.T.);
#407=FACE_OUTER_BOUND('',#661,.T.);
#408=FACE_OUTER_BOUND('',#662,.T.);
#409=FACE_OUTER_BOUND('',#663,.T.);
#410=FACE_OUTER_BOUND('',#664,.T.);
#411=FACE_OUTER_BOUND('',#665,.T.);
#412=FACE_OUTER_BOUND('',#666,.T.);
#413=FACE_OUTER_BOUND('',#667,.T.);
#414=FACE_OUTER_BOUND('',#668,.T.);
#415=FACE_OUTER_BOUND('',#669,.T.);
#416=FACE_OUTER_BOUND('',#670,.T.);
#417=FACE_OUTER_BOUND('',#671,.T.);
#418=FACE_OUTER_BOUND('',#672,.T.);
#419=FACE_OUTER_BOUND('',#673,.T.);
#420=FACE_OUTER_BOUND('',#674,.T.);
#421=FACE_OUTER_BOUND('',#675,.T.);
#422=FACE_OUTER_BOUND('',#676,.T.);
#423=FACE_OUTER_BOUND('',#677,.T.);
#424=FACE_OUTER_BOUND('',#678,.T.);
#425=FACE_OUTER_BOUND('',#679,.T.);
#426=FACE_OUTER_BOUND('',#680,.T.);
#427=FACE_OUTER_BOUND('',#681,.T.);
#428=FACE_OUTER_BOUND('',#682,.T.);
#429=FACE_OUTER_BOUND('',#683,.T.);
#430=FACE_OUTER_BOUND('',#684,.T.);
#431=FACE_OUTER_BOUND('',#685,.T.);
#432=FACE_OUTER_BOUND('',#686,.T.);
#433=FACE_OUTER_BOUND('',#687,.T.);
#434=FACE_OUTER_BOUND('',#688,.T.);
#435=FACE_OUTER_BOUND('',#689,.T.);
#436=FACE_OUTER_BOUND('',#690,.T.);
#437=FACE_OUTER_BOUND('',#691,.T.);
#438=FACE_OUTER_BOUND('',#692,.T.);
#439=FACE_OUTER_BOUND('',#693,.T.);
#440=FACE_OUTER_BOUND('',#694,.T.);
#441=FACE_OUTER_BOUND('',#695,.T.);
#442=FACE_OUTER_BOUND('',#696,.T.);
#443=FACE_OUTER_BOUND('',#697,.T.);
#444=FACE_OUTER_BOUND('',#698,.T.);
#445=FACE_OUTER_BOUND('',#699,.T.);
#446=FACE_OUTER_BOUND('',#700,.T.);
#447=FACE_OUTER_BOUND('',#701,.T.);
#448=FACE_OUTER_BOUND('',#702,.T.);
#449=FACE_OUTER_BOUND('',#703,.T.);
#450=FACE_OUTER_BOUND('',#704,.T.);
#451=FACE_OUTER_BOUND('',#705,.T.);
#452=FACE_OUTER_BOUND('',#706,.T.);
#453=FACE_OUTER_BOUND('',#707,.T.);
#454=FACE_OUTER_BOUND('',#708,.T.);
#455=FACE_OUTER_BOUND('',#709,.T.);
#456=FACE_OUTER_BOUND('',#710,.T.);
#457=FACE_OUTER_BOUND('',#711,.T.);
#458=FACE_OUTER_BOUND('',#712,.T.);
#459=FACE_OUTER_BOUND('',#713,.T.);
#460=FACE_OUTER_BOUND('',#714,.T.);
#461=FACE_OUTER_BOUND('',#715,.T.);
#462=FACE_OUTER_BOUND('',#716,.T.);
#463=FACE_OUTER_BOUND('',#717,.T.);
#464=FACE_OUTER_BOUND('',#718,.T.);
#465=FACE_OUTER_BOUND('',#719,.T.);
#466=FACE_OUTER_BOUND('',#720,.T.);
#467=FACE_OUTER_BOUND('',#721,.T.);
#468=FACE_OUTER_BOUND('',#722,.T.);
#469=FACE_OUTER_BOUND('',#723,.T.);
#470=FACE_OUTER_BOUND('',#724,.T.);
#471=FACE_OUTER_BOUND('',#725,.T.);
#472=FACE_OUTER_BOUND('',#726,.T.);
#473=FACE_OUTER_BOUND('',#727,.T.);
#474=FACE_OUTER_BOUND('',#729,.T.);
#475=FACE_OUTER_BOUND('',#731,.T.);
#645=EDGE_LOOP('',(#2728,#2729,#2730,#2731));
#646=EDGE_LOOP('',(#2732));
#647=EDGE_LOOP('',(#2733,#2734,#2735,#2736));
#648=EDGE_LOOP('',(#2737,#2738,#2739,#2740));
#649=EDGE_LOOP('',(#2741,#2742,#2743,#2744));
#650=EDGE_LOOP('',(#2745,#2746,#2747,#2748));
#651=EDGE_LOOP('',(#2749,#2750,#2751,#2752));
#652=EDGE_LOOP('',(#2753,#2754,#2755,#2756));
#653=EDGE_LOOP('',(#2757,#2758,#2759,#2760));
#654=EDGE_LOOP('',(#2761,#2762,#2763,#2764));
#655=EDGE_LOOP('',(#2765,#2766,#2767,#2768));
#656=EDGE_LOOP('',(#2769,#2770,#2771,#2772));
#657=EDGE_LOOP('',(#2773,#2774,#2775,#2776));
#658=EDGE_LOOP('',(#2777,#2778,#2779,#2780));
#659=EDGE_LOOP('',(#2781,#2782,#2783,#2784));
#660=EDGE_LOOP('',(#2785,#2786,#2787,#2788));
#661=EDGE_LOOP('',(#2789,#2790,#2791,#2792));
#662=EDGE_LOOP('',(#2793,#2794,#2795,#2796));
#663=EDGE_LOOP('',(#2797,#2798,#2799,#2800));
#664=EDGE_LOOP('',(#2801,#2802,#2803,#2804));
#665=EDGE_LOOP('',(#2805,#2806,#2807,#2808));
#666=EDGE_LOOP('',(#2809,#2810,#2811,#2812,#2813,#2814));
#667=EDGE_LOOP('',(#2815,#2816,#2817,#2818));
#668=EDGE_LOOP('',(#2819,#2820,#2821,#2822));
#669=EDGE_LOOP('',(#2823,#2824,#2825,#2826));
#670=EDGE_LOOP('',(#2827,#2828,#2829,#2830));
#671=EDGE_LOOP('',(#2831,#2832,#2833,#2834));
#672=EDGE_LOOP('',(#2835,#2836,#2837,#2838));
#673=EDGE_LOOP('',(#2839,#2840,#2841,#2842));
#674=EDGE_LOOP('',(#2843,#2844,#2845,#2846));
#675=EDGE_LOOP('',(#2847,#2848,#2849,#2850));
#676=EDGE_LOOP('',(#2851,#2852,#2853,#2854));
#677=EDGE_LOOP('',(#2855,#2856,#2857,#2858));
#678=EDGE_LOOP('',(#2859,#2860,#2861,#2862));
#679=EDGE_LOOP('',(#2863,#2864,#2865,#2866));
#680=EDGE_LOOP('',(#2867,#2868,#2869,#2870));
#681=EDGE_LOOP('',(#2871,#2872,#2873,#2874));
#682=EDGE_LOOP('',(#2875,#2876,#2877,#2878));
#683=EDGE_LOOP('',(#2879,#2880,#2881,#2882));
#684=EDGE_LOOP('',(#2883,#2884,#2885,#2886));
#685=EDGE_LOOP('',(#2887,#2888,#2889,#2890));
#686=EDGE_LOOP('',(#2891,#2892,#2893,#2894));
#687=EDGE_LOOP('',(#2895,#2896,#2897,#2898));
#688=EDGE_LOOP('',(#2899,#2900,#2901,#2902));
#689=EDGE_LOOP('',(#2903,#2904,#2905,#2906));
#690=EDGE_LOOP('',(#2907,#2908,#2909,#2910));
#691=EDGE_LOOP('',(#2911,#2912,#2913,#2914));
#692=EDGE_LOOP('',(#2915,#2916,#2917,#2918));
#693=EDGE_LOOP('',(#2919,#2920,#2921,#2922));
#694=EDGE_LOOP('',(#2923,#2924,#2925,#2926));
#695=EDGE_LOOP('',(#2927,#2928,#2929,#2930));
#696=EDGE_LOOP('',(#2931,#2932,#2933,#2934));
#697=EDGE_LOOP('',(#2935,#2936,#2937,#2938));
#698=EDGE_LOOP('',(#2939,#2940,#2941,#2942));
#699=EDGE_LOOP('',(#2943,#2944,#2945,#2946));
#700=EDGE_LOOP('',(#2947,#2948,#2949,#2950));
#701=EDGE_LOOP('',(#2951,#2952,#2953,#2954));
#702=EDGE_LOOP('',(#2955,#2956,#2957,#2958));
#703=EDGE_LOOP('',(#2959,#2960,#2961,#2962));
#704=EDGE_LOOP('',(#2963,#2964,#2965,#2966,#2967,#2968,#2969,#2970,#2971,
#2972,#2973,#2974,#2975,#2976,#2977,#2978,#2979,#2980,#2981,#2982,#2983,
#2984,#2985,#2986,#2987,#2988,#2989,#2990,#2991,#2992,#2993,#2994,#2995,
#2996,#2997,#2998,#2999,#3000,#3001,#3002,#3003,#3004,#3005,#3006,#3007,
#3008,#3009,#3010,#3011,#3012,#3013,#3014,#3015,#3016,#3017,#3018,#3019,
#3020,#3021,#3022,#3023,#3024,#3025,#3026,#3027,#3028,#3029,#3030,#3031,
#3032,#3033,#3034,#3035,#3036,#3037,#3038,#3039,#3040,#3041,#3042,#3043,
#3044,#3045,#3046));
#705=EDGE_LOOP('',(#3047,#3048,#3049,#3050));
#706=EDGE_LOOP('',(#3051,#3052,#3053,#3054));
#707=EDGE_LOOP('',(#3055,#3056,#3057,#3058));
#708=EDGE_LOOP('',(#3059,#3060,#3061,#3062));
#709=EDGE_LOOP('',(#3063,#3064,#3065,#3066));
#710=EDGE_LOOP('',(#3067,#3068,#3069,#3070));
#711=EDGE_LOOP('',(#3071,#3072,#3073,#3074));
#712=EDGE_LOOP('',(#3075,#3076,#3077,#3078));
#713=EDGE_LOOP('',(#3079,#3080,#3081,#3082));
#714=EDGE_LOOP('',(#3083,#3084,#3085,#3086));
#715=EDGE_LOOP('',(#3087,#3088,#3089,#3090));
#716=EDGE_LOOP('',(#3091,#3092,#3093,#3094));
#717=EDGE_LOOP('',(#3095,#3096,#3097,#3098));
#718=EDGE_LOOP('',(#3099,#3100,#3101,#3102));
#719=EDGE_LOOP('',(#3103,#3104,#3105,#3106));
#720=EDGE_LOOP('',(#3107,#3108,#3109,#3110));
#721=EDGE_LOOP('',(#3111,#3112,#3113,#3114));
#722=EDGE_LOOP('',(#3115,#3116,#3117,#3118));
#723=EDGE_LOOP('',(#3119,#3120,#3121,#3122));
#724=EDGE_LOOP('',(#3123,#3124,#3125,#3126));
#725=EDGE_LOOP('',(#3127,#3128,#3129,#3130));
#726=EDGE_LOOP('',(#3131,#3132,#3133,#3134));
#727=EDGE_LOOP('',(#3135,#3136,#3137,#3138,#3139,#3140,#3141,#3142,#3143,
#3144,#3145,#3146,#3147,#3148,#3149,#3150,#3151,#3152,#3153,#3154,#3155,
#3156,#3157,#3158,#3159,#3160,#3161,#3162,#3163,#3164,#3165,#3166,#3167,
#3168,#3169,#3170,#3171,#3172,#3173,#3174,#3175,#3176,#3177,#3178,#3179,
#3180,#3181,#3182,#3183,#3184,#3185,#3186,#3187,#3188,#3189,#3190,#3191,
#3192,#3193,#3194,#3195,#3196,#3197,#3198,#3199,#3200,#3201,#3202,#3203,
#3204,#3205,#3206,#3207,#3208,#3209,#3210,#3211,#3212,#3213,#3214,#3215,
#3216,#3217,#3218));
#728=EDGE_LOOP('',(#3219));
#729=EDGE_LOOP('',(#3220));
#730=EDGE_LOOP('',(#3221));
#731=EDGE_LOOP('',(#3222,#3223,#3224,#3225));
#891=CIRCLE('',#4050,0.75);
#892=CIRCLE('',#4072,25.);
#893=CIRCLE('',#4073,34.);
#894=CIRCLE('',#4074,34.);
#895=CIRCLE('',#4075,25.);
#896=CIRCLE('',#4077,25.);
#897=CIRCLE('',#4078,34.);
#898=CIRCLE('',#4080,25.);
#899=CIRCLE('',#4081,34.);
#900=CIRCLE('',#4083,25.);
#901=CIRCLE('',#4084,34.);
#902=CIRCLE('',#4086,25.);
#903=CIRCLE('',#4087,34.);
#904=CIRCLE('',#4089,25.);
#905=CIRCLE('',#4090,34.);
#906=CIRCLE('',#4092,25.);
#907=CIRCLE('',#4093,34.);
#908=CIRCLE('',#4095,25.);
#909=CIRCLE('',#4096,34.);
#910=CIRCLE('',#4098,25.);
#911=CIRCLE('',#4099,34.);
#912=CIRCLE('',#4101,25.);
#913=CIRCLE('',#4102,34.);
#914=CIRCLE('',#4104,25.);
#915=CIRCLE('',#4105,34.);
#916=CIRCLE('',#4107,25.);
#917=CIRCLE('',#4108,34.);
#918=CIRCLE('',#4110,25.);
#919=CIRCLE('',#4111,34.);
#920=CIRCLE('',#4113,25.);
#921=CIRCLE('',#4114,34.);
#922=CIRCLE('',#4116,25.);
#923=CIRCLE('',#4117,34.);
#924=CIRCLE('',#4119,25.);
#925=CIRCLE('',#4120,34.);
#926=CIRCLE('',#4122,25.);
#927=CIRCLE('',#4123,34.);
#928=CIRCLE('',#4125,25.);
#929=CIRCLE('',#4126,34.);
#930=CIRCLE('',#4128,25.);
#931=CIRCLE('',#4129,34.);
#932=CIRCLE('',#4150,25.);
#933=CIRCLE('',#4151,25.);
#934=CIRCLE('',#4152,25.);
#935=CIRCLE('',#4153,25.);
#936=CIRCLE('',#4154,25.);
#937=CIRCLE('',#4155,25.);
#938=CIRCLE('',#4156,25.);
#939=CIRCLE('',#4157,25.);
#940=CIRCLE('',#4158,25.);
#941=CIRCLE('',#4159,25.);
#942=CIRCLE('',#4160,25.);
#943=CIRCLE('',#4161,25.);
#944=CIRCLE('',#4162,25.);
#945=CIRCLE('',#4163,25.);
#946=CIRCLE('',#4164,25.);
#947=CIRCLE('',#4165,25.);
#948=CIRCLE('',#4166,25.);
#949=CIRCLE('',#4167,25.);
#950=CIRCLE('',#4168,25.);
#951=CIRCLE('',#4169,25.);
#952=CIRCLE('',#4170,25.);
#953=CIRCLE('',#4171,25.);
#954=CIRCLE('',#4173,34.);
#955=CIRCLE('',#4175,34.);
#956=CIRCLE('',#4177,34.);
#957=CIRCLE('',#4179,34.);
#958=CIRCLE('',#4181,34.);
#959=CIRCLE('',#4183,34.);
#960=CIRCLE('',#4185,34.);
#961=CIRCLE('',#4187,34.);
#962=CIRCLE('',#4189,34.);
#963=CIRCLE('',#4191,34.);
#964=CIRCLE('',#4193,34.);
#965=CIRCLE('',#4195,34.);
#966=CIRCLE('',#4197,34.);
#967=CIRCLE('',#4199,34.);
#968=CIRCLE('',#4201,34.);
#969=CIRCLE('',#4203,34.);
#970=CIRCLE('',#4205,34.);
#971=CIRCLE('',#4207,34.);
#972=CIRCLE('',#4209,34.);
#973=CIRCLE('',#4212,34.);
#974=CIRCLE('',#4215,34.);
#975=CIRCLE('',#4216,34.);
#1085=LINE('',#5928,#1371);
#1086=LINE('',#5934,#1372);
#1087=LINE('',#5936,#1373);
#1088=LINE('',#5938,#1374);
#1089=LINE('',#5939,#1375);
#1090=LINE('',#5943,#1376);
#1091=LINE('',#5945,#1377);
#1092=LINE('',#5947,#1378);
#1093=LINE('',#5948,#1379);
#1094=LINE('',#5952,#1380);
#1095=LINE('',#5954,#1381);
#1096=LINE('',#5956,#1382);
#1097=LINE('',#5957,#1383);
#1098=LINE('',#5961,#1384);
#1099=LINE('',#5963,#1385);
#1100=LINE('',#5965,#1386);
#1101=LINE('',#5966,#1387);
#1102=LINE('',#5970,#1388);
#1103=LINE('',#5972,#1389);
#1104=LINE('',#5974,#1390);
#1105=LINE('',#5975,#1391);
#1106=LINE('',#5979,#1392);
#1107=LINE('',#5981,#1393);
#1108=LINE('',#5983,#1394);
#1109=LINE('',#5984,#1395);
#1110=LINE('',#5988,#1396);
#1111=LINE('',#5990,#1397);
#1112=LINE('',#5992,#1398);
#1113=LINE('',#5993,#1399);
#1114=LINE('',#5997,#1400);
#1115=LINE('',#5999,#1401);
#1116=LINE('',#6001,#1402);
#1117=LINE('',#6002,#1403);
#1118=LINE('',#6006,#1404);
#1119=LINE('',#6008,#1405);
#1120=LINE('',#6010,#1406);
#1121=LINE('',#6011,#1407);
#1122=LINE('',#6015,#1408);
#1123=LINE('',#6017,#1409);
#1124=LINE('',#6019,#1410);
#1125=LINE('',#6020,#1411);
#1126=LINE('',#6024,#1412);
#1127=LINE('',#6026,#1413);
#1128=LINE('',#6028,#1414);
#1129=LINE('',#6029,#1415);
#1130=LINE('',#6033,#1416);
#1131=LINE('',#6035,#1417);
#1132=LINE('',#6037,#1418);
#1133=LINE('',#6038,#1419);
#1134=LINE('',#6042,#1420);
#1135=LINE('',#6044,#1421);
#1136=LINE('',#6046,#1422);
#1137=LINE('',#6047,#1423);
#1138=LINE('',#6051,#1424);
#1139=LINE('',#6053,#1425);
#1140=LINE('',#6055,#1426);
#1141=LINE('',#6056,#1427);
#1142=LINE('',#6060,#1428);
#1143=LINE('',#6062,#1429);
#1144=LINE('',#6064,#1430);
#1145=LINE('',#6065,#1431);
#1146=LINE('',#6069,#1432);
#1147=LINE('',#6071,#1433);
#1148=LINE('',#6073,#1434);
#1149=LINE('',#6074,#1435);
#1150=LINE('',#6078,#1436);
#1151=LINE('',#6080,#1437);
#1152=LINE('',#6082,#1438);
#1153=LINE('',#6083,#1439);
#1154=LINE('',#6087,#1440);
#1155=LINE('',#6089,#1441);
#1156=LINE('',#6091,#1442);
#1157=LINE('',#6092,#1443);
#1158=LINE('',#6096,#1444);
#1159=LINE('',#6098,#1445);
#1160=LINE('',#6100,#1446);
#1161=LINE('',#6101,#1447);
#1162=LINE('',#6107,#1448);
#1163=LINE('',#6116,#1449);
#1164=LINE('',#6122,#1450);
#1165=LINE('',#6128,#1451);
#1166=LINE('',#6134,#1452);
#1167=LINE('',#6140,#1453);
#1168=LINE('',#6146,#1454);
#1169=LINE('',#6152,#1455);
#1170=LINE('',#6158,#1456);
#1171=LINE('',#6164,#1457);
#1172=LINE('',#6170,#1458);
#1173=LINE('',#6176,#1459);
#1174=LINE('',#6182,#1460);
#1175=LINE('',#6188,#1461);
#1176=LINE('',#6194,#1462);
#1177=LINE('',#6200,#1463);
#1178=LINE('',#6206,#1464);
#1179=LINE('',#6212,#1465);
#1180=LINE('',#6218,#1466);
#1181=LINE('',#6222,#1467);
#1182=LINE('',#6224,#1468);
#1183=LINE('',#6225,#1469);
#1184=LINE('',#6228,#1470);
#1185=LINE('',#6230,#1471);
#1186=LINE('',#6231,#1472);
#1187=LINE('',#6234,#1473);
#1188=LINE('',#6236,#1474);
#1189=LINE('',#6237,#1475);
#1190=LINE('',#6240,#1476);
#1191=LINE('',#6242,#1477);
#1192=LINE('',#6243,#1478);
#1193=LINE('',#6246,#1479);
#1194=LINE('',#6248,#1480);
#1195=LINE('',#6249,#1481);
#1196=LINE('',#6252,#1482);
#1197=LINE('',#6254,#1483);
#1198=LINE('',#6255,#1484);
#1199=LINE('',#6258,#1485);
#1200=LINE('',#6260,#1486);
#1201=LINE('',#6261,#1487);
#1202=LINE('',#6264,#1488);
#1203=LINE('',#6266,#1489);
#1204=LINE('',#6267,#1490);
#1205=LINE('',#6270,#1491);
#1206=LINE('',#6272,#1492);
#1207=LINE('',#6273,#1493);
#1208=LINE('',#6276,#1494);
#1209=LINE('',#6278,#1495);
#1210=LINE('',#6279,#1496);
#1211=LINE('',#6282,#1497);
#1212=LINE('',#6284,#1498);
#1213=LINE('',#6285,#1499);
#1214=LINE('',#6288,#1500);
#1215=LINE('',#6290,#1501);
#1216=LINE('',#6291,#1502);
#1217=LINE('',#6294,#1503);
#1218=LINE('',#6296,#1504);
#1219=LINE('',#6297,#1505);
#1220=LINE('',#6300,#1506);
#1221=LINE('',#6302,#1507);
#1222=LINE('',#6303,#1508);
#1223=LINE('',#6306,#1509);
#1224=LINE('',#6308,#1510);
#1225=LINE('',#6309,#1511);
#1226=LINE('',#6312,#1512);
#1227=LINE('',#6314,#1513);
#1228=LINE('',#6315,#1514);
#1229=LINE('',#6318,#1515);
#1230=LINE('',#6320,#1516);
#1231=LINE('',#6321,#1517);
#1232=LINE('',#6324,#1518);
#1233=LINE('',#6326,#1519);
#1234=LINE('',#6327,#1520);
#1235=LINE('',#6330,#1521);
#1236=LINE('',#6332,#1522);
#1237=LINE('',#6333,#1523);
#1238=LINE('',#6337,#1524);
#1239=LINE('',#6345,#1525);
#1240=LINE('',#6349,#1526);
#1241=LINE('',#6368,#1527);
#1242=LINE('',#6381,#1528);
#1243=LINE('',#6409,#1529);
#1244=LINE('',#6410,#1530);
#1245=LINE('',#6413,#1531);
#1246=LINE('',#6416,#1532);
#1247=LINE('',#6420,#1533);
#1371=VECTOR('',#4700,0.75);
#1372=VECTOR('',#4707,10.);
#1373=VECTOR('',#4708,10.);
#1374=VECTOR('',#4709,10.);
#1375=VECTOR('',#4710,10.);
#1376=VECTOR('',#4713,10.);
#1377=VECTOR('',#4714,10.);
#1378=VECTOR('',#4715,10.);
#1379=VECTOR('',#4716,10.);
#1380=VECTOR('',#4719,10.);
#1381=VECTOR('',#4720,10.);
#1382=VECTOR('',#4721,10.);
#1383=VECTOR('',#4722,10.);
#1384=VECTOR('',#4725,10.);
#1385=VECTOR('',#4726,10.);
#1386=VECTOR('',#4727,10.);
#1387=VECTOR('',#4728,10.);
#1388=VECTOR('',#4731,10.);
#1389=VECTOR('',#4732,10.);
#1390=VECTOR('',#4733,10.);
#1391=VECTOR('',#4734,10.);
#1392=VECTOR('',#4737,10.);
#1393=VECTOR('',#4738,10.);
#1394=VECTOR('',#4739,10.);
#1395=VECTOR('',#4740,10.);
#1396=VECTOR('',#4743,10.);
#1397=VECTOR('',#4744,10.);
#1398=VECTOR('',#4745,10.);
#1399=VECTOR('',#4746,10.);
#1400=VECTOR('',#4749,10.);
#1401=VECTOR('',#4750,10.);
#1402=VECTOR('',#4751,10.);
#1403=VECTOR('',#4752,10.);
#1404=VECTOR('',#4755,10.);
#1405=VECTOR('',#4756,10.);
#1406=VECTOR('',#4757,10.);
#1407=VECTOR('',#4758,10.);
#1408=VECTOR('',#4761,10.);
#1409=VECTOR('',#4762,10.);
#1410=VECTOR('',#4763,10.);
#1411=VECTOR('',#4764,10.);
#1412=VECTOR('',#4767,10.);
#1413=VECTOR('',#4768,10.);
#1414=VECTOR('',#4769,10.);
#1415=VECTOR('',#4770,10.);
#1416=VECTOR('',#4773,10.);
#1417=VECTOR('',#4774,10.);
#1418=VECTOR('',#4775,10.);
#1419=VECTOR('',#4776,10.);
#1420=VECTOR('',#4779,10.);
#1421=VECTOR('',#4780,10.);
#1422=VECTOR('',#4781,10.);
#1423=VECTOR('',#4782,10.);
#1424=VECTOR('',#4785,10.);
#1425=VECTOR('',#4786,10.);
#1426=VECTOR('',#4787,10.);
#1427=VECTOR('',#4788,10.);
#1428=VECTOR('',#4791,10.);
#1429=VECTOR('',#4792,10.);
#1430=VECTOR('',#4793,10.);
#1431=VECTOR('',#4794,10.);
#1432=VECTOR('',#4797,10.);
#1433=VECTOR('',#4798,10.);
#1434=VECTOR('',#4799,10.);
#1435=VECTOR('',#4800,10.);
#1436=VECTOR('',#4803,10.);
#1437=VECTOR('',#4804,10.);
#1438=VECTOR('',#4805,10.);
#1439=VECTOR('',#4806,10.);
#1440=VECTOR('',#4809,10.);
#1441=VECTOR('',#4810,10.);
#1442=VECTOR('',#4811,10.);
#1443=VECTOR('',#4812,10.);
#1444=VECTOR('',#4815,10.);
#1445=VECTOR('',#4816,10.);
#1446=VECTOR('',#4817,10.);
#1447=VECTOR('',#4818,10.);
#1448=VECTOR('',#4823,10.);
#1449=VECTOR('',#4834,10.);
#1450=VECTOR('',#4841,10.);
#1451=VECTOR('',#4848,10.);
#1452=VECTOR('',#4855,10.);
#1453=VECTOR('',#4862,10.);
#1454=VECTOR('',#4869,10.);
#1455=VECTOR('',#4876,10.);
#1456=VECTOR('',#4883,10.);
#1457=VECTOR('',#4890,10.);
#1458=VECTOR('',#4897,10.);
#1459=VECTOR('',#4904,10.);
#1460=VECTOR('',#4911,10.);
#1461=VECTOR('',#4918,10.);
#1462=VECTOR('',#4925,10.);
#1463=VECTOR('',#4932,10.);
#1464=VECTOR('',#4939,10.);
#1465=VECTOR('',#4946,10.);
#1466=VECTOR('',#4953,10.);
#1467=VECTOR('',#4958,10.);
#1468=VECTOR('',#4959,10.);
#1469=VECTOR('',#4960,10.);
#1470=VECTOR('',#4963,10.);
#1471=VECTOR('',#4964,10.);
#1472=VECTOR('',#4965,10.);
#1473=VECTOR('',#4968,10.);
#1474=VECTOR('',#4969,10.);
#1475=VECTOR('',#4970,10.);
#1476=VECTOR('',#4973,10.);
#1477=VECTOR('',#4974,10.);
#1478=VECTOR('',#4975,10.);
#1479=VECTOR('',#4978,10.);
#1480=VECTOR('',#4979,10.);
#1481=VECTOR('',#4980,10.);
#1482=VECTOR('',#4983,10.);
#1483=VECTOR('',#4984,10.);
#1484=VECTOR('',#4985,10.);
#1485=VECTOR('',#4988,10.);
#1486=VECTOR('',#4989,10.);
#1487=VECTOR('',#4990,10.);
#1488=VECTOR('',#4993,10.);
#1489=VECTOR('',#4994,10.);
#1490=VECTOR('',#4995,10.);
#1491=VECTOR('',#4998,10.);
#1492=VECTOR('',#4999,10.);
#1493=VECTOR('',#5000,10.);
#1494=VECTOR('',#5003,10.);
#1495=VECTOR('',#5004,10.);
#1496=VECTOR('',#5005,10.);
#1497=VECTOR('',#5008,10.);
#1498=VECTOR('',#5009,10.);
#1499=VECTOR('',#5010,10.);
#1500=VECTOR('',#5013,10.);
#1501=VECTOR('',#5014,10.);
#1502=VECTOR('',#5015,10.);
#1503=VECTOR('',#5018,10.);
#1504=VECTOR('',#5019,10.);
#1505=VECTOR('',#5020,10.);
#1506=VECTOR('',#5023,10.);
#1507=VECTOR('',#5024,10.);
#1508=VECTOR('',#5025,10.);
#1509=VECTOR('',#5028,10.);
#1510=VECTOR('',#5029,10.);
#1511=VECTOR('',#5030,10.);
#1512=VECTOR('',#5033,10.);
#1513=VECTOR('',#5034,10.);
#1514=VECTOR('',#5035,10.);
#1515=VECTOR('',#5038,10.);
#1516=VECTOR('',#5039,10.);
#1517=VECTOR('',#5040,10.);
#1518=VECTOR('',#5043,10.);
#1519=VECTOR('',#5044,10.);
#1520=VECTOR('',#5045,10.);
#1521=VECTOR('',#5048,10.);
#1522=VECTOR('',#5049,10.);
#1523=VECTOR('',#5050,10.);
#1524=VECTOR('',#5055,25.);
#1525=VECTOR('',#5066,10.);
#1526=VECTOR('',#5069,10.);
#1527=VECTOR('',#5104,10.);
#1528=VECTOR('',#5127,10.);
#1529=VECTOR('',#5180,10.);
#1530=VECTOR('',#5181,10.);
#1531=VECTOR('',#5184,10.);
#1532=VECTOR('',#5189,10.);
#1533=VECTOR('',#5194,34.);
#1695=VERTEX_POINT('',#5892);
#1696=VERTEX_POINT('',#5927);
#1697=VERTEX_POINT('',#5932);
#1698=VERTEX_POINT('',#5933);
#1699=VERTEX_POINT('',#5935);
#1700=VERTEX_POINT('',#5937);
#1701=VERTEX_POINT('',#5941);
#1702=VERTEX_POINT('',#5942);
#1703=VERTEX_POINT('',#5944);
#1704=VERTEX_POINT('',#5946);
#1705=VERTEX_POINT('',#5950);
#1706=VERTEX_POINT('',#5951);
#1707=VERTEX_POINT('',#5953);
#1708=VERTEX_POINT('',#5955);
#1709=VERTEX_POINT('',#5959);
#1710=VERTEX_POINT('',#5960);
#1711=VERTEX_POINT('',#5962);
#1712=VERTEX_POINT('',#5964);
#1713=VERTEX_POINT('',#5968);
#1714=VERTEX_POINT('',#5969);
#1715=VERTEX_POINT('',#5971);
#1716=VERTEX_POINT('',#5973);
#1717=VERTEX_POINT('',#5977);
#1718=VERTEX_POINT('',#5978);
#1719=VERTEX_POINT('',#5980);
#1720=VERTEX_POINT('',#5982);
#1721=VERTEX_POINT('',#5986);
#1722=VERTEX_POINT('',#5987);
#1723=VERTEX_POINT('',#5989);
#1724=VERTEX_POINT('',#5991);
#1725=VERTEX_POINT('',#5995);
#1726=VERTEX_POINT('',#5996);
#1727=VERTEX_POINT('',#5998);
#1728=VERTEX_POINT('',#6000);
#1729=VERTEX_POINT('',#6004);
#1730=VERTEX_POINT('',#6005);
#1731=VERTEX_POINT('',#6007);
#1732=VERTEX_POINT('',#6009);
#1733=VERTEX_POINT('',#6013);
#1734=VERTEX_POINT('',#6014);
#1735=VERTEX_POINT('',#6016);
#1736=VERTEX_POINT('',#6018);
#1737=VERTEX_POINT('',#6022);
#1738=VERTEX_POINT('',#6023);
#1739=VERTEX_POINT('',#6025);
#1740=VERTEX_POINT('',#6027);
#1741=VERTEX_POINT('',#6031);
#1742=VERTEX_POINT('',#6032);
#1743=VERTEX_POINT('',#6034);
#1744=VERTEX_POINT('',#6036);
#1745=VERTEX_POINT('',#6040);
#1746=VERTEX_POINT('',#6041);
#1747=VERTEX_POINT('',#6043);
#1748=VERTEX_POINT('',#6045);
#1749=VERTEX_POINT('',#6049);
#1750=VERTEX_POINT('',#6050);
#1751=VERTEX_POINT('',#6052);
#1752=VERTEX_POINT('',#6054);
#1753=VERTEX_POINT('',#6058);
#1754=VERTEX_POINT('',#6059);
#1755=VERTEX_POINT('',#6061);
#1756=VERTEX_POINT('',#6063);
#1757=VERTEX_POINT('',#6067);
#1758=VERTEX_POINT('',#6068);
#1759=VERTEX_POINT('',#6070);
#1760=VERTEX_POINT('',#6072);
#1761=VERTEX_POINT('',#6076);
#1762=VERTEX_POINT('',#6077);
#1763=VERTEX_POINT('',#6079);
#1764=VERTEX_POINT('',#6081);
#1765=VERTEX_POINT('',#6085);
#1766=VERTEX_POINT('',#6086);
#1767=VERTEX_POINT('',#6088);
#1768=VERTEX_POINT('',#6090);
#1769=VERTEX_POINT('',#6094);
#1770=VERTEX_POINT('',#6095);
#1771=VERTEX_POINT('',#6097);
#1772=VERTEX_POINT('',#6099);
#1773=VERTEX_POINT('',#6103);
#1774=VERTEX_POINT('',#6104);
#1775=VERTEX_POINT('',#6106);
#1776=VERTEX_POINT('',#6108);
#1777=VERTEX_POINT('',#6113);
#1778=VERTEX_POINT('',#6115);
#1779=VERTEX_POINT('',#6119);
#1780=VERTEX_POINT('',#6121);
#1781=VERTEX_POINT('',#6125);
#1782=VERTEX_POINT('',#6127);
#1783=VERTEX_POINT('',#6131);
#1784=VERTEX_POINT('',#6133);
#1785=VERTEX_POINT('',#6137);
#1786=VERTEX_POINT('',#6139);
#1787=VERTEX_POINT('',#6143);
#1788=VERTEX_POINT('',#6145);
#1789=VERTEX_POINT('',#6149);
#1790=VERTEX_POINT('',#6151);
#1791=VERTEX_POINT('',#6155);
#1792=VERTEX_POINT('',#6157);
#1793=VERTEX_POINT('',#6161);
#1794=VERTEX_POINT('',#6163);
#1795=VERTEX_POINT('',#6167);
#1796=VERTEX_POINT('',#6169);
#1797=VERTEX_POINT('',#6173);
#1798=VERTEX_POINT('',#6175);
#1799=VERTEX_POINT('',#6179);
#1800=VERTEX_POINT('',#6181);
#1801=VERTEX_POINT('',#6185);
#1802=VERTEX_POINT('',#6187);
#1803=VERTEX_POINT('',#6191);
#1804=VERTEX_POINT('',#6193);
#1805=VERTEX_POINT('',#6197);
#1806=VERTEX_POINT('',#6199);
#1807=VERTEX_POINT('',#6203);
#1808=VERTEX_POINT('',#6205);
#1809=VERTEX_POINT('',#6209);
#1810=VERTEX_POINT('',#6211);
#1811=VERTEX_POINT('',#6215);
#1812=VERTEX_POINT('',#6217);
#1813=VERTEX_POINT('',#6221);
#1814=VERTEX_POINT('',#6223);
#1815=VERTEX_POINT('',#6227);
#1816=VERTEX_POINT('',#6229);
#1817=VERTEX_POINT('',#6233);
#1818=VERTEX_POINT('',#6235);
#1819=VERTEX_POINT('',#6239);
#1820=VERTEX_POINT('',#6241);
#1821=VERTEX_POINT('',#6245);
#1822=VERTEX_POINT('',#6247);
#1823=VERTEX_POINT('',#6251);
#1824=VERTEX_POINT('',#6253);
#1825=VERTEX_POINT('',#6257);
#1826=VERTEX_POINT('',#6259);
#1827=VERTEX_POINT('',#6263);
#1828=VERTEX_POINT('',#6265);
#1829=VERTEX_POINT('',#6269);
#1830=VERTEX_POINT('',#6271);
#1831=VERTEX_POINT('',#6275);
#1832=VERTEX_POINT('',#6277);
#1833=VERTEX_POINT('',#6281);
#1834=VERTEX_POINT('',#6283);
#1835=VERTEX_POINT('',#6287);
#1836=VERTEX_POINT('',#6289);
#1837=VERTEX_POINT('',#6293);
#1838=VERTEX_POINT('',#6295);
#1839=VERTEX_POINT('',#6299);
#1840=VERTEX_POINT('',#6301);
#1841=VERTEX_POINT('',#6305);
#1842=VERTEX_POINT('',#6307);
#1843=VERTEX_POINT('',#6311);
#1844=VERTEX_POINT('',#6313);
#1845=VERTEX_POINT('',#6317);
#1846=VERTEX_POINT('',#6319);
#1847=VERTEX_POINT('',#6323);
#1848=VERTEX_POINT('',#6325);
#1849=VERTEX_POINT('',#6329);
#1850=VERTEX_POINT('',#6331);
#1851=VERTEX_POINT('',#6335);
#1852=VERTEX_POINT('',#6342);
#1853=VERTEX_POINT('',#6344);
#1854=VERTEX_POINT('',#6346);
#1855=VERTEX_POINT('',#6348);
#1856=VERTEX_POINT('',#6366);
#1857=VERTEX_POINT('',#6380);
#1858=VERTEX_POINT('',#6408);
#1859=VERTEX_POINT('',#6412);
#1860=VERTEX_POINT('',#6418);
#2081=EDGE_CURVE('',#1695,#1695,#69,.T.);
#2082=EDGE_CURVE('',#1695,#1696,#1085,.T.);
#2083=EDGE_CURVE('',#1696,#1696,#891,.T.);
#2084=EDGE_CURVE('',#1697,#1698,#1086,.T.);
#2085=EDGE_CURVE('',#1699,#1697,#1087,.T.);
#2086=EDGE_CURVE('',#1700,#1699,#1088,.T.);
#2087=EDGE_CURVE('',#1698,#1700,#1089,.T.);
#2088=EDGE_CURVE('',#1701,#1702,#1090,.T.);
#2089=EDGE_CURVE('',#1703,#1701,#1091,.T.);
#2090=EDGE_CURVE('',#1704,#1703,#1092,.T.);
#2091=EDGE_CURVE('',#1702,#1704,#1093,.T.);
#2092=EDGE_CURVE('',#1705,#1706,#1094,.T.);
#2093=EDGE_CURVE('',#1707,#1705,#1095,.T.);
#2094=EDGE_CURVE('',#1708,#1707,#1096,.T.);
#2095=EDGE_CURVE('',#1706,#1708,#1097,.T.);
#2096=EDGE_CURVE('',#1709,#1710,#1098,.T.);
#2097=EDGE_CURVE('',#1711,#1709,#1099,.T.);
#2098=EDGE_CURVE('',#1712,#1711,#1100,.T.);
#2099=EDGE_CURVE('',#1710,#1712,#1101,.T.);
#2100=EDGE_CURVE('',#1713,#1714,#1102,.T.);
#2101=EDGE_CURVE('',#1715,#1713,#1103,.T.);
#2102=EDGE_CURVE('',#1716,#1715,#1104,.T.);
#2103=EDGE_CURVE('',#1714,#1716,#1105,.T.);
#2104=EDGE_CURVE('',#1717,#1718,#1106,.T.);
#2105=EDGE_CURVE('',#1719,#1717,#1107,.T.);
#2106=EDGE_CURVE('',#1720,#1719,#1108,.T.);
#2107=EDGE_CURVE('',#1718,#1720,#1109,.T.);
#2108=EDGE_CURVE('',#1721,#1722,#1110,.T.);
#2109=EDGE_CURVE('',#1723,#1721,#1111,.T.);
#2110=EDGE_CURVE('',#1724,#1723,#1112,.T.);
#2111=EDGE_CURVE('',#1722,#1724,#1113,.T.);
#2112=EDGE_CURVE('',#1725,#1726,#1114,.T.);
#2113=EDGE_CURVE('',#1727,#1725,#1115,.T.);
#2114=EDGE_CURVE('',#1728,#1727,#1116,.T.);
#2115=EDGE_CURVE('',#1726,#1728,#1117,.T.);
#2116=EDGE_CURVE('',#1729,#1730,#1118,.T.);
#2117=EDGE_CURVE('',#1731,#1729,#1119,.T.);
#2118=EDGE_CURVE('',#1732,#1731,#1120,.T.);
#2119=EDGE_CURVE('',#1730,#1732,#1121,.T.);
#2120=EDGE_CURVE('',#1733,#1734,#1122,.T.);
#2121=EDGE_CURVE('',#1735,#1733,#1123,.T.);
#2122=EDGE_CURVE('',#1736,#1735,#1124,.T.);
#2123=EDGE_CURVE('',#1734,#1736,#1125,.T.);
#2124=EDGE_CURVE('',#1737,#1738,#1126,.T.);
#2125=EDGE_CURVE('',#1739,#1737,#1127,.T.);
#2126=EDGE_CURVE('',#1740,#1739,#1128,.T.);
#2127=EDGE_CURVE('',#1738,#1740,#1129,.T.);
#2128=EDGE_CURVE('',#1741,#1742,#1130,.T.);
#2129=EDGE_CURVE('',#1743,#1741,#1131,.T.);
#2130=EDGE_CURVE('',#1744,#1743,#1132,.T.);
#2131=EDGE_CURVE('',#1742,#1744,#1133,.T.);
#2132=EDGE_CURVE('',#1745,#1746,#1134,.T.);
#2133=EDGE_CURVE('',#1747,#1745,#1135,.T.);
#2134=EDGE_CURVE('',#1748,#1747,#1136,.T.);
#2135=EDGE_CURVE('',#1746,#1748,#1137,.T.);
#2136=EDGE_CURVE('',#1749,#1750,#1138,.T.);
#2137=EDGE_CURVE('',#1751,#1749,#1139,.T.);
#2138=EDGE_CURVE('',#1752,#1751,#1140,.T.);
#2139=EDGE_CURVE('',#1750,#1752,#1141,.T.);
#2140=EDGE_CURVE('',#1753,#1754,#1142,.T.);
#2141=EDGE_CURVE('',#1755,#1753,#1143,.T.);
#2142=EDGE_CURVE('',#1756,#1755,#1144,.T.);
#2143=EDGE_CURVE('',#1754,#1756,#1145,.T.);
#2144=EDGE_CURVE('',#1757,#1758,#1146,.T.);
#2145=EDGE_CURVE('',#1759,#1757,#1147,.T.);
#2146=EDGE_CURVE('',#1760,#1759,#1148,.T.);
#2147=EDGE_CURVE('',#1758,#1760,#1149,.T.);
#2148=EDGE_CURVE('',#1761,#1762,#1150,.T.);
#2149=EDGE_CURVE('',#1763,#1761,#1151,.T.);
#2150=EDGE_CURVE('',#1764,#1763,#1152,.T.);
#2151=EDGE_CURVE('',#1762,#1764,#1153,.T.);
#2152=EDGE_CURVE('',#1765,#1766,#1154,.T.);
#2153=EDGE_CURVE('',#1767,#1765,#1155,.T.);
#2154=EDGE_CURVE('',#1768,#1767,#1156,.T.);
#2155=EDGE_CURVE('',#1766,#1768,#1157,.T.);
#2156=EDGE_CURVE('',#1769,#1770,#1158,.T.);
#2157=EDGE_CURVE('',#1771,#1769,#1159,.T.);
#2158=EDGE_CURVE('',#1772,#1771,#1160,.T.);
#2159=EDGE_CURVE('',#1770,#1772,#1161,.T.);
#2160=EDGE_CURVE('',#1773,#1774,#892,.T.);
#2161=EDGE_CURVE('',#1773,#1775,#1162,.T.);
#2162=EDGE_CURVE('',#1776,#1775,#893,.T.);
#2163=EDGE_CURVE('',#1771,#1776,#894,.T.);
#2164=EDGE_CURVE('',#1774,#1769,#895,.T.);
#2165=EDGE_CURVE('',#1777,#1765,#896,.T.);
#2166=EDGE_CURVE('',#1777,#1778,#1163,.T.);
#2167=EDGE_CURVE('',#1767,#1778,#897,.T.);
#2168=EDGE_CURVE('',#1779,#1761,#898,.T.);
#2169=EDGE_CURVE('',#1779,#1780,#1164,.T.);
#2170=EDGE_CURVE('',#1763,#1780,#899,.T.);
#2171=EDGE_CURVE('',#1781,#1757,#900,.T.);
#2172=EDGE_CURVE('',#1781,#1782,#1165,.T.);
#2173=EDGE_CURVE('',#1759,#1782,#901,.T.);
#2174=EDGE_CURVE('',#1783,#1753,#902,.T.);
#2175=EDGE_CURVE('',#1783,#1784,#1166,.T.);
#2176=EDGE_CURVE('',#1755,#1784,#903,.T.);
#2177=EDGE_CURVE('',#1785,#1749,#904,.T.);
#2178=EDGE_CURVE('',#1785,#1786,#1167,.T.);
#2179=EDGE_CURVE('',#1751,#1786,#905,.T.);
#2180=EDGE_CURVE('',#1787,#1745,#906,.T.);
#2181=EDGE_CURVE('',#1787,#1788,#1168,.T.);
#2182=EDGE_CURVE('',#1747,#1788,#907,.T.);
#2183=EDGE_CURVE('',#1789,#1741,#908,.T.);
#2184=EDGE_CURVE('',#1789,#1790,#1169,.T.);
#2185=EDGE_CURVE('',#1743,#1790,#909,.T.);
#2186=EDGE_CURVE('',#1791,#1737,#910,.T.);
#2187=EDGE_CURVE('',#1791,#1792,#1170,.T.);
#2188=EDGE_CURVE('',#1739,#1792,#911,.T.);
#2189=EDGE_CURVE('',#1793,#1733,#912,.T.);
#2190=EDGE_CURVE('',#1793,#1794,#1171,.T.);
#2191=EDGE_CURVE('',#1735,#1794,#913,.T.);
#2192=EDGE_CURVE('',#1795,#1729,#914,.T.);
#2193=EDGE_CURVE('',#1795,#1796,#1172,.T.);
#2194=EDGE_CURVE('',#1731,#1796,#915,.T.);
#2195=EDGE_CURVE('',#1797,#1725,#916,.T.);
#2196=EDGE_CURVE('',#1797,#1798,#1173,.T.);
#2197=EDGE_CURVE('',#1727,#1798,#917,.T.);
#2198=EDGE_CURVE('',#1799,#1721,#918,.T.);
#2199=EDGE_CURVE('',#1799,#1800,#1174,.T.);
#2200=EDGE_CURVE('',#1723,#1800,#919,.T.);
#2201=EDGE_CURVE('',#1801,#1717,#920,.T.);
#2202=EDGE_CURVE('',#1801,#1802,#1175,.T.);
#2203=EDGE_CURVE('',#1719,#1802,#921,.T.);
#2204=EDGE_CURVE('',#1803,#1713,#922,.T.);
#2205=EDGE_CURVE('',#1803,#1804,#1176,.T.);
#2206=EDGE_CURVE('',#1715,#1804,#923,.T.);
#2207=EDGE_CURVE('',#1805,#1709,#924,.T.);
#2208=EDGE_CURVE('',#1805,#1806,#1177,.T.);
#2209=EDGE_CURVE('',#1711,#1806,#925,.T.);
#2210=EDGE_CURVE('',#1807,#1705,#926,.T.);
#2211=EDGE_CURVE('',#1807,#1808,#1178,.T.);
#2212=EDGE_CURVE('',#1707,#1808,#927,.T.);
#2213=EDGE_CURVE('',#1809,#1701,#928,.T.);
#2214=EDGE_CURVE('',#1809,#1810,#1179,.T.);
#2215=EDGE_CURVE('',#1703,#1810,#929,.T.);
#2216=EDGE_CURVE('',#1811,#1697,#930,.T.);
#2217=EDGE_CURVE('',#1811,#1812,#1180,.T.);
#2218=EDGE_CURVE('',#1699,#1812,#931,.T.);
#2219=EDGE_CURVE('',#1813,#1785,#1181,.T.);
#2220=EDGE_CURVE('',#1814,#1813,#1182,.T.);
#2221=EDGE_CURVE('',#1786,#1814,#1183,.T.);
#2222=EDGE_CURVE('',#1815,#1801,#1184,.T.);
#2223=EDGE_CURVE('',#1816,#1815,#1185,.T.);
#2224=EDGE_CURVE('',#1802,#1816,#1186,.T.);
#2225=EDGE_CURVE('',#1817,#1803,#1187,.T.);
#2226=EDGE_CURVE('',#1818,#1817,#1188,.T.);
#2227=EDGE_CURVE('',#1804,#1818,#1189,.T.);
#2228=EDGE_CURVE('',#1819,#1783,#1190,.T.);
#2229=EDGE_CURVE('',#1820,#1819,#1191,.T.);
#2230=EDGE_CURVE('',#1784,#1820,#1192,.T.);
#2231=EDGE_CURVE('',#1821,#1811,#1193,.T.);
#2232=EDGE_CURVE('',#1822,#1821,#1194,.T.);
#2233=EDGE_CURVE('',#1812,#1822,#1195,.T.);
#2234=EDGE_CURVE('',#1823,#1799,#1196,.T.);
#2235=EDGE_CURVE('',#1824,#1823,#1197,.T.);
#2236=EDGE_CURVE('',#1800,#1824,#1198,.T.);
#2237=EDGE_CURVE('',#1825,#1781,#1199,.T.);
#2238=EDGE_CURVE('',#1826,#1825,#1200,.T.);
#2239=EDGE_CURVE('',#1782,#1826,#1201,.T.);
#2240=EDGE_CURVE('',#1827,#1779,#1202,.T.);
#2241=EDGE_CURVE('',#1828,#1827,#1203,.T.);
#2242=EDGE_CURVE('',#1780,#1828,#1204,.T.);
#2243=EDGE_CURVE('',#1829,#1797,#1205,.T.);
#2244=EDGE_CURVE('',#1830,#1829,#1206,.T.);
#2245=EDGE_CURVE('',#1798,#1830,#1207,.T.);
#2246=EDGE_CURVE('',#1831,#1795,#1208,.T.);
#2247=EDGE_CURVE('',#1832,#1831,#1209,.T.);
#2248=EDGE_CURVE('',#1796,#1832,#1210,.T.);
#2249=EDGE_CURVE('',#1833,#1777,#1211,.T.);
#2250=EDGE_CURVE('',#1834,#1833,#1212,.T.);
#2251=EDGE_CURVE('',#1778,#1834,#1213,.T.);
#2252=EDGE_CURVE('',#1835,#1773,#1214,.T.);
#2253=EDGE_CURVE('',#1836,#1835,#1215,.T.);
#2254=EDGE_CURVE('',#1775,#1836,#1216,.T.);
#2255=EDGE_CURVE('',#1837,#1793,#1217,.T.);
#2256=EDGE_CURVE('',#1838,#1837,#1218,.T.);
#2257=EDGE_CURVE('',#1794,#1838,#1219,.T.);
#2258=EDGE_CURVE('',#1839,#1791,#1220,.T.);
#2259=EDGE_CURVE('',#1840,#1839,#1221,.T.);
#2260=EDGE_CURVE('',#1792,#1840,#1222,.T.);
#2261=EDGE_CURVE('',#1841,#1809,#1223,.T.);
#2262=EDGE_CURVE('',#1842,#1841,#1224,.T.);
#2263=EDGE_CURVE('',#1810,#1842,#1225,.T.);
#2264=EDGE_CURVE('',#1843,#1807,#1226,.T.);
#2265=EDGE_CURVE('',#1844,#1843,#1227,.T.);
#2266=EDGE_CURVE('',#1808,#1844,#1228,.T.);
#2267=EDGE_CURVE('',#1845,#1789,#1229,.T.);
#2268=EDGE_CURVE('',#1846,#1845,#1230,.T.);
#2269=EDGE_CURVE('',#1790,#1846,#1231,.T.);
#2270=EDGE_CURVE('',#1847,#1805,#1232,.T.);
#2271=EDGE_CURVE('',#1848,#1847,#1233,.T.);
#2272=EDGE_CURVE('',#1806,#1848,#1234,.T.);
#2273=EDGE_CURVE('',#1849,#1787,#1235,.T.);
#2274=EDGE_CURVE('',#1850,#1849,#1236,.T.);
#2275=EDGE_CURVE('',#1788,#1850,#1237,.T.);
#2276=EDGE_CURVE('',#1851,#1851,#932,.T.);
#2277=EDGE_CURVE('',#1851,#1774,#1238,.T.);
#2278=EDGE_CURVE('',#1770,#1833,#933,.T.);
#2279=EDGE_CURVE('',#1766,#1827,#934,.T.);
#2280=EDGE_CURVE('',#1762,#1825,#935,.T.);
#2281=EDGE_CURVE('',#1758,#1819,#936,.T.);
#2282=EDGE_CURVE('',#1754,#1852,#937,.T.);
#2283=EDGE_CURVE('',#1852,#1853,#1239,.T.);
#2284=EDGE_CURVE('',#1853,#1854,#938,.T.);
#2285=EDGE_CURVE('',#1854,#1855,#1240,.T.);
#2286=EDGE_CURVE('',#1855,#1813,#939,.T.);
#2287=EDGE_CURVE('',#1750,#1849,#940,.T.);
#2288=EDGE_CURVE('',#1746,#1845,#941,.T.);
#2289=EDGE_CURVE('',#1742,#1839,#942,.T.);
#2290=EDGE_CURVE('',#1738,#1837,#943,.T.);
#2291=EDGE_CURVE('',#1734,#1831,#944,.T.);
#2292=EDGE_CURVE('',#1730,#1829,#945,.T.);
#2293=EDGE_CURVE('',#1726,#1823,#946,.T.);
#2294=EDGE_CURVE('',#1722,#1821,#947,.T.);
#2295=EDGE_CURVE('',#1698,#1815,#948,.T.);
#2296=EDGE_CURVE('',#1718,#1817,#949,.T.);
#2297=EDGE_CURVE('',#1714,#1847,#950,.T.);
#2298=EDGE_CURVE('',#1710,#1843,#951,.T.);
#2299=EDGE_CURVE('',#1706,#1841,#952,.T.);
#2300=EDGE_CURVE('',#1702,#1835,#953,.T.);
#2301=EDGE_CURVE('',#1856,#1756,#954,.T.);
#2302=EDGE_CURVE('',#1856,#1852,#1241,.T.);
#2303=EDGE_CURVE('',#1836,#1704,#955,.T.);
#2304=EDGE_CURVE('',#1834,#1772,#956,.T.);
#2305=EDGE_CURVE('',#1828,#1768,#957,.T.);
#2306=EDGE_CURVE('',#1826,#1764,#958,.T.);
#2307=EDGE_CURVE('',#1820,#1760,#959,.T.);
#2308=EDGE_CURVE('',#1855,#1857,#1242,.T.);
#2309=EDGE_CURVE('',#1814,#1857,#960,.T.);
#2310=EDGE_CURVE('',#1850,#1752,#961,.T.);
#2311=EDGE_CURVE('',#1846,#1748,#962,.T.);
#2312=EDGE_CURVE('',#1840,#1744,#963,.T.);
#2313=EDGE_CURVE('',#1838,#1740,#964,.T.);
#2314=EDGE_CURVE('',#1832,#1736,#965,.T.);
#2315=EDGE_CURVE('',#1830,#1732,#966,.T.);
#2316=EDGE_CURVE('',#1824,#1728,#967,.T.);
#2317=EDGE_CURVE('',#1816,#1700,#968,.T.);
#2318=EDGE_CURVE('',#1818,#1720,#969,.T.);
#2319=EDGE_CURVE('',#1848,#1716,#970,.T.);
#2320=EDGE_CURVE('',#1844,#1712,#971,.T.);
#2321=EDGE_CURVE('',#1842,#1708,#972,.T.);
#2322=EDGE_CURVE('',#1858,#1854,#1243,.T.);
#2323=EDGE_CURVE('',#1857,#1858,#1244,.T.);
#2324=EDGE_CURVE('',#1853,#1859,#1245,.T.);
#2325=EDGE_CURVE('',#1858,#1859,#973,.T.);
#2326=EDGE_CURVE('',#1859,#1856,#1246,.T.);
#2327=EDGE_CURVE('',#1860,#1860,#974,.T.);
#2328=EDGE_CURVE('',#1860,#1776,#1247,.T.);
#2329=EDGE_CURVE('',#1822,#1724,#975,.T.);
#2728=ORIENTED_EDGE('',*,*,#2081,.F.);
#2729=ORIENTED_EDGE('',*,*,#2082,.T.);
#2730=ORIENTED_EDGE('',*,*,#2083,.T.);
#2731=ORIENTED_EDGE('',*,*,#2082,.F.);
#2732=ORIENTED_EDGE('',*,*,#2083,.F.);
#2733=ORIENTED_EDGE('',*,*,#2084,.F.);
#2734=ORIENTED_EDGE('',*,*,#2085,.F.);
#2735=ORIENTED_EDGE('',*,*,#2086,.F.);
#2736=ORIENTED_EDGE('',*,*,#2087,.F.);
#2737=ORIENTED_EDGE('',*,*,#2088,.F.);
#2738=ORIENTED_EDGE('',*,*,#2089,.F.);
#2739=ORIENTED_EDGE('',*,*,#2090,.F.);
#2740=ORIENTED_EDGE('',*,*,#2091,.F.);
#2741=ORIENTED_EDGE('',*,*,#2092,.F.);
#2742=ORIENTED_EDGE('',*,*,#2093,.F.);
#2743=ORIENTED_EDGE('',*,*,#2094,.F.);
#2744=ORIENTED_EDGE('',*,*,#2095,.F.);
#2745=ORIENTED_EDGE('',*,*,#2096,.F.);
#2746=ORIENTED_EDGE('',*,*,#2097,.F.);
#2747=ORIENTED_EDGE('',*,*,#2098,.F.);
#2748=ORIENTED_EDGE('',*,*,#2099,.F.);
#2749=ORIENTED_EDGE('',*,*,#2100,.F.);
#2750=ORIENTED_EDGE('',*,*,#2101,.F.);
#2751=ORIENTED_EDGE('',*,*,#2102,.F.);
#2752=ORIENTED_EDGE('',*,*,#2103,.F.);
#2753=ORIENTED_EDGE('',*,*,#2104,.F.);
#2754=ORIENTED_EDGE('',*,*,#2105,.F.);
#2755=ORIENTED_EDGE('',*,*,#2106,.F.);
#2756=ORIENTED_EDGE('',*,*,#2107,.F.);
#2757=ORIENTED_EDGE('',*,*,#2108,.F.);
#2758=ORIENTED_EDGE('',*,*,#2109,.F.);
#2759=ORIENTED_EDGE('',*,*,#2110,.F.);
#2760=ORIENTED_EDGE('',*,*,#2111,.F.);
#2761=ORIENTED_EDGE('',*,*,#2112,.F.);
#2762=ORIENTED_EDGE('',*,*,#2113,.F.);
#2763=ORIENTED_EDGE('',*,*,#2114,.F.);
#2764=ORIENTED_EDGE('',*,*,#2115,.F.);
#2765=ORIENTED_EDGE('',*,*,#2116,.F.);
#2766=ORIENTED_EDGE('',*,*,#2117,.F.);
#2767=ORIENTED_EDGE('',*,*,#2118,.F.);
#2768=ORIENTED_EDGE('',*,*,#2119,.F.);
#2769=ORIENTED_EDGE('',*,*,#2120,.F.);
#2770=ORIENTED_EDGE('',*,*,#2121,.F.);
#2771=ORIENTED_EDGE('',*,*,#2122,.F.);
#2772=ORIENTED_EDGE('',*,*,#2123,.F.);
#2773=ORIENTED_EDGE('',*,*,#2124,.F.);
#2774=ORIENTED_EDGE('',*,*,#2125,.F.);
#2775=ORIENTED_EDGE('',*,*,#2126,.F.);
#2776=ORIENTED_EDGE('',*,*,#2127,.F.);
#2777=ORIENTED_EDGE('',*,*,#2128,.F.);
#2778=ORIENTED_EDGE('',*,*,#2129,.F.);
#2779=ORIENTED_EDGE('',*,*,#2130,.F.);
#2780=ORIENTED_EDGE('',*,*,#2131,.F.);
#2781=ORIENTED_EDGE('',*,*,#2132,.F.);
#2782=ORIENTED_EDGE('',*,*,#2133,.F.);
#2783=ORIENTED_EDGE('',*,*,#2134,.F.);
#2784=ORIENTED_EDGE('',*,*,#2135,.F.);
#2785=ORIENTED_EDGE('',*,*,#2136,.F.);
#2786=ORIENTED_EDGE('',*,*,#2137,.F.);
#2787=ORIENTED_EDGE('',*,*,#2138,.F.);
#2788=ORIENTED_EDGE('',*,*,#2139,.F.);
#2789=ORIENTED_EDGE('',*,*,#2140,.F.);
#2790=ORIENTED_EDGE('',*,*,#2141,.F.);
#2791=ORIENTED_EDGE('',*,*,#2142,.F.);
#2792=ORIENTED_EDGE('',*,*,#2143,.F.);
#2793=ORIENTED_EDGE('',*,*,#2144,.F.);
#2794=ORIENTED_EDGE('',*,*,#2145,.F.);
#2795=ORIENTED_EDGE('',*,*,#2146,.F.);
#2796=ORIENTED_EDGE('',*,*,#2147,.F.);
#2797=ORIENTED_EDGE('',*,*,#2148,.F.);
#2798=ORIENTED_EDGE('',*,*,#2149,.F.);
#2799=ORIENTED_EDGE('',*,*,#2150,.F.);
#2800=ORIENTED_EDGE('',*,*,#2151,.F.);
#2801=ORIENTED_EDGE('',*,*,#2152,.F.);
#2802=ORIENTED_EDGE('',*,*,#2153,.F.);
#2803=ORIENTED_EDGE('',*,*,#2154,.F.);
#2804=ORIENTED_EDGE('',*,*,#2155,.F.);
#2805=ORIENTED_EDGE('',*,*,#2156,.F.);
#2806=ORIENTED_EDGE('',*,*,#2157,.F.);
#2807=ORIENTED_EDGE('',*,*,#2158,.F.);
#2808=ORIENTED_EDGE('',*,*,#2159,.F.);
#2809=ORIENTED_EDGE('',*,*,#2160,.F.);
#2810=ORIENTED_EDGE('',*,*,#2161,.T.);
#2811=ORIENTED_EDGE('',*,*,#2162,.F.);
#2812=ORIENTED_EDGE('',*,*,#2163,.F.);
#2813=ORIENTED_EDGE('',*,*,#2157,.T.);
#2814=ORIENTED_EDGE('',*,*,#2164,.F.);
#2815=ORIENTED_EDGE('',*,*,#2165,.F.);
#2816=ORIENTED_EDGE('',*,*,#2166,.T.);
#2817=ORIENTED_EDGE('',*,*,#2167,.F.);
#2818=ORIENTED_EDGE('',*,*,#2153,.T.);
#2819=ORIENTED_EDGE('',*,*,#2168,.F.);
#2820=ORIENTED_EDGE('',*,*,#2169,.T.);
#2821=ORIENTED_EDGE('',*,*,#2170,.F.);
#2822=ORIENTED_EDGE('',*,*,#2149,.T.);
#2823=ORIENTED_EDGE('',*,*,#2171,.F.);
#2824=ORIENTED_EDGE('',*,*,#2172,.T.);
#2825=ORIENTED_EDGE('',*,*,#2173,.F.);
#2826=ORIENTED_EDGE('',*,*,#2145,.T.);
#2827=ORIENTED_EDGE('',*,*,#2174,.F.);
#2828=ORIENTED_EDGE('',*,*,#2175,.T.);
#2829=ORIENTED_EDGE('',*,*,#2176,.F.);
#2830=ORIENTED_EDGE('',*,*,#2141,.T.);
#2831=ORIENTED_EDGE('',*,*,#2177,.F.);
#2832=ORIENTED_EDGE('',*,*,#2178,.T.);
#2833=ORIENTED_EDGE('',*,*,#2179,.F.);
#2834=ORIENTED_EDGE('',*,*,#2137,.T.);
#2835=ORIENTED_EDGE('',*,*,#2180,.F.);
#2836=ORIENTED_EDGE('',*,*,#2181,.T.);
#2837=ORIENTED_EDGE('',*,*,#2182,.F.);
#2838=ORIENTED_EDGE('',*,*,#2133,.T.);
#2839=ORIENTED_EDGE('',*,*,#2183,.F.);
#2840=ORIENTED_EDGE('',*,*,#2184,.T.);
#2841=ORIENTED_EDGE('',*,*,#2185,.F.);
#2842=ORIENTED_EDGE('',*,*,#2129,.T.);
#2843=ORIENTED_EDGE('',*,*,#2186,.F.);
#2844=ORIENTED_EDGE('',*,*,#2187,.T.);
#2845=ORIENTED_EDGE('',*,*,#2188,.F.);
#2846=ORIENTED_EDGE('',*,*,#2125,.T.);
#2847=ORIENTED_EDGE('',*,*,#2189,.F.);
#2848=ORIENTED_EDGE('',*,*,#2190,.T.);
#2849=ORIENTED_EDGE('',*,*,#2191,.F.);
#2850=ORIENTED_EDGE('',*,*,#2121,.T.);
#2851=ORIENTED_EDGE('',*,*,#2192,.F.);
#2852=ORIENTED_EDGE('',*,*,#2193,.T.);
#2853=ORIENTED_EDGE('',*,*,#2194,.F.);
#2854=ORIENTED_EDGE('',*,*,#2117,.T.);
#2855=ORIENTED_EDGE('',*,*,#2195,.F.);
#2856=ORIENTED_EDGE('',*,*,#2196,.T.);
#2857=ORIENTED_EDGE('',*,*,#2197,.F.);
#2858=ORIENTED_EDGE('',*,*,#2113,.T.);
#2859=ORIENTED_EDGE('',*,*,#2198,.F.);
#2860=ORIENTED_EDGE('',*,*,#2199,.T.);
#2861=ORIENTED_EDGE('',*,*,#2200,.F.);
#2862=ORIENTED_EDGE('',*,*,#2109,.T.);
#2863=ORIENTED_EDGE('',*,*,#2201,.F.);
#2864=ORIENTED_EDGE('',*,*,#2202,.T.);
#2865=ORIENTED_EDGE('',*,*,#2203,.F.);
#2866=ORIENTED_EDGE('',*,*,#2105,.T.);
#2867=ORIENTED_EDGE('',*,*,#2204,.F.);
#2868=ORIENTED_EDGE('',*,*,#2205,.T.);
#2869=ORIENTED_EDGE('',*,*,#2206,.F.);
#2870=ORIENTED_EDGE('',*,*,#2101,.T.);
#2871=ORIENTED_EDGE('',*,*,#2207,.F.);
#2872=ORIENTED_EDGE('',*,*,#2208,.T.);
#2873=ORIENTED_EDGE('',*,*,#2209,.F.);
#2874=ORIENTED_EDGE('',*,*,#2097,.T.);
#2875=ORIENTED_EDGE('',*,*,#2210,.F.);
#2876=ORIENTED_EDGE('',*,*,#2211,.T.);
#2877=ORIENTED_EDGE('',*,*,#2212,.F.);
#2878=ORIENTED_EDGE('',*,*,#2093,.T.);
#2879=ORIENTED_EDGE('',*,*,#2213,.F.);
#2880=ORIENTED_EDGE('',*,*,#2214,.T.);
#2881=ORIENTED_EDGE('',*,*,#2215,.F.);
#2882=ORIENTED_EDGE('',*,*,#2089,.T.);
#2883=ORIENTED_EDGE('',*,*,#2216,.F.);
#2884=ORIENTED_EDGE('',*,*,#2217,.T.);
#2885=ORIENTED_EDGE('',*,*,#2218,.F.);
#2886=ORIENTED_EDGE('',*,*,#2085,.T.);
#2887=ORIENTED_EDGE('',*,*,#2219,.F.);
#2888=ORIENTED_EDGE('',*,*,#2220,.F.);
#2889=ORIENTED_EDGE('',*,*,#2221,.F.);
#2890=ORIENTED_EDGE('',*,*,#2178,.F.);
#2891=ORIENTED_EDGE('',*,*,#2222,.F.);
#2892=ORIENTED_EDGE('',*,*,#2223,.F.);
#2893=ORIENTED_EDGE('',*,*,#2224,.F.);
#2894=ORIENTED_EDGE('',*,*,#2202,.F.);
#2895=ORIENTED_EDGE('',*,*,#2225,.F.);
#2896=ORIENTED_EDGE('',*,*,#2226,.F.);
#2897=ORIENTED_EDGE('',*,*,#2227,.F.);
#2898=ORIENTED_EDGE('',*,*,#2205,.F.);
#2899=ORIENTED_EDGE('',*,*,#2228,.F.);
#2900=ORIENTED_EDGE('',*,*,#2229,.F.);
#2901=ORIENTED_EDGE('',*,*,#2230,.F.);
#2902=ORIENTED_EDGE('',*,*,#2175,.F.);
#2903=ORIENTED_EDGE('',*,*,#2231,.F.);
#2904=ORIENTED_EDGE('',*,*,#2232,.F.);
#2905=ORIENTED_EDGE('',*,*,#2233,.F.);
#2906=ORIENTED_EDGE('',*,*,#2217,.F.);
#2907=ORIENTED_EDGE('',*,*,#2234,.F.);
#2908=ORIENTED_EDGE('',*,*,#2235,.F.);
#2909=ORIENTED_EDGE('',*,*,#2236,.F.);
#2910=ORIENTED_EDGE('',*,*,#2199,.F.);
#2911=ORIENTED_EDGE('',*,*,#2237,.F.);
#2912=ORIENTED_EDGE('',*,*,#2238,.F.);
#2913=ORIENTED_EDGE('',*,*,#2239,.F.);
#2914=ORIENTED_EDGE('',*,*,#2172,.F.);
#2915=ORIENTED_EDGE('',*,*,#2240,.F.);
#2916=ORIENTED_EDGE('',*,*,#2241,.F.);
#2917=ORIENTED_EDGE('',*,*,#2242,.F.);
#2918=ORIENTED_EDGE('',*,*,#2169,.F.);
#2919=ORIENTED_EDGE('',*,*,#2243,.F.);
#2920=ORIENTED_EDGE('',*,*,#2244,.F.);
#2921=ORIENTED_EDGE('',*,*,#2245,.F.);
#2922=ORIENTED_EDGE('',*,*,#2196,.F.);
#2923=ORIENTED_EDGE('',*,*,#2246,.F.);
#2924=ORIENTED_EDGE('',*,*,#2247,.F.);
#2925=ORIENTED_EDGE('',*,*,#2248,.F.);
#2926=ORIENTED_EDGE('',*,*,#2193,.F.);
#2927=ORIENTED_EDGE('',*,*,#2249,.F.);
#2928=ORIENTED_EDGE('',*,*,#2250,.F.);
#2929=ORIENTED_EDGE('',*,*,#2251,.F.);
#2930=ORIENTED_EDGE('',*,*,#2166,.F.);
#2931=ORIENTED_EDGE('',*,*,#2252,.F.);
#2932=ORIENTED_EDGE('',*,*,#2253,.F.);
#2933=ORIENTED_EDGE('',*,*,#2254,.F.);
#2934=ORIENTED_EDGE('',*,*,#2161,.F.);
#2935=ORIENTED_EDGE('',*,*,#2255,.F.);
#2936=ORIENTED_EDGE('',*,*,#2256,.F.);
#2937=ORIENTED_EDGE('',*,*,#2257,.F.);
#2938=ORIENTED_EDGE('',*,*,#2190,.F.);
#2939=ORIENTED_EDGE('',*,*,#2258,.F.);
#2940=ORIENTED_EDGE('',*,*,#2259,.F.);
#2941=ORIENTED_EDGE('',*,*,#2260,.F.);
#2942=ORIENTED_EDGE('',*,*,#2187,.F.);
#2943=ORIENTED_EDGE('',*,*,#2261,.F.);
#2944=ORIENTED_EDGE('',*,*,#2262,.F.);
#2945=ORIENTED_EDGE('',*,*,#2263,.F.);
#2946=ORIENTED_EDGE('',*,*,#2214,.F.);
#2947=ORIENTED_EDGE('',*,*,#2264,.F.);
#2948=ORIENTED_EDGE('',*,*,#2265,.F.);
#2949=ORIENTED_EDGE('',*,*,#2266,.F.);
#2950=ORIENTED_EDGE('',*,*,#2211,.F.);
#2951=ORIENTED_EDGE('',*,*,#2267,.F.);
#2952=ORIENTED_EDGE('',*,*,#2268,.F.);
#2953=ORIENTED_EDGE('',*,*,#2269,.F.);
#2954=ORIENTED_EDGE('',*,*,#2184,.F.);
#2955=ORIENTED_EDGE('',*,*,#2270,.F.);
#2956=ORIENTED_EDGE('',*,*,#2271,.F.);
#2957=ORIENTED_EDGE('',*,*,#2272,.F.);
#2958=ORIENTED_EDGE('',*,*,#2208,.F.);
#2959=ORIENTED_EDGE('',*,*,#2273,.F.);
#2960=ORIENTED_EDGE('',*,*,#2274,.F.);
#2961=ORIENTED_EDGE('',*,*,#2275,.F.);
#2962=ORIENTED_EDGE('',*,*,#2181,.F.);
#2963=ORIENTED_EDGE('',*,*,#2276,.F.);
#2964=ORIENTED_EDGE('',*,*,#2277,.T.);
#2965=ORIENTED_EDGE('',*,*,#2164,.T.);
#2966=ORIENTED_EDGE('',*,*,#2156,.T.);
#2967=ORIENTED_EDGE('',*,*,#2278,.T.);
#2968=ORIENTED_EDGE('',*,*,#2249,.T.);
#2969=ORIENTED_EDGE('',*,*,#2165,.T.);
#2970=ORIENTED_EDGE('',*,*,#2152,.T.);
#2971=ORIENTED_EDGE('',*,*,#2279,.T.);
#2972=ORIENTED_EDGE('',*,*,#2240,.T.);
#2973=ORIENTED_EDGE('',*,*,#2168,.T.);
#2974=ORIENTED_EDGE('',*,*,#2148,.T.);
#2975=ORIENTED_EDGE('',*,*,#2280,.T.);
#2976=ORIENTED_EDGE('',*,*,#2237,.T.);
#2977=ORIENTED_EDGE('',*,*,#2171,.T.);
#2978=ORIENTED_EDGE('',*,*,#2144,.T.);
#2979=ORIENTED_EDGE('',*,*,#2281,.T.);
#2980=ORIENTED_EDGE('',*,*,#2228,.T.);
#2981=ORIENTED_EDGE('',*,*,#2174,.T.);
#2982=ORIENTED_EDGE('',*,*,#2140,.T.);
#2983=ORIENTED_EDGE('',*,*,#2282,.T.);
#2984=ORIENTED_EDGE('',*,*,#2283,.T.);
#2985=ORIENTED_EDGE('',*,*,#2284,.T.);
#2986=ORIENTED_EDGE('',*,*,#2285,.T.);
#2987=ORIENTED_EDGE('',*,*,#2286,.T.);
#2988=ORIENTED_EDGE('',*,*,#2219,.T.);
#2989=ORIENTED_EDGE('',*,*,#2177,.T.);
#2990=ORIENTED_EDGE('',*,*,#2136,.T.);
#2991=ORIENTED_EDGE('',*,*,#2287,.T.);
#2992=ORIENTED_EDGE('',*,*,#2273,.T.);
#2993=ORIENTED_EDGE('',*,*,#2180,.T.);
#2994=ORIENTED_EDGE('',*,*,#2132,.T.);
#2995=ORIENTED_EDGE('',*,*,#2288,.T.);
#2996=ORIENTED_EDGE('',*,*,#2267,.T.);
#2997=ORIENTED_EDGE('',*,*,#2183,.T.);
#2998=ORIENTED_EDGE('',*,*,#2128,.T.);
#2999=ORIENTED_EDGE('',*,*,#2289,.T.);
#3000=ORIENTED_EDGE('',*,*,#2258,.T.);
#3001=ORIENTED_EDGE('',*,*,#2186,.T.);
#3002=ORIENTED_EDGE('',*,*,#2124,.T.);
#3003=ORIENTED_EDGE('',*,*,#2290,.T.);
#3004=ORIENTED_EDGE('',*,*,#2255,.T.);
#3005=ORIENTED_EDGE('',*,*,#2189,.T.);
#3006=ORIENTED_EDGE('',*,*,#2120,.T.);
#3007=ORIENTED_EDGE('',*,*,#2291,.T.);
#3008=ORIENTED_EDGE('',*,*,#2246,.T.);
#3009=ORIENTED_EDGE('',*,*,#2192,.T.);
#3010=ORIENTED_EDGE('',*,*,#2116,.T.);
#3011=ORIENTED_EDGE('',*,*,#2292,.T.);
#3012=ORIENTED_EDGE('',*,*,#2243,.T.);
#3013=ORIENTED_EDGE('',*,*,#2195,.T.);
#3014=ORIENTED_EDGE('',*,*,#2112,.T.);
#3015=ORIENTED_EDGE('',*,*,#2293,.T.);
#3016=ORIENTED_EDGE('',*,*,#2234,.T.);
#3017=ORIENTED_EDGE('',*,*,#2198,.T.);
#3018=ORIENTED_EDGE('',*,*,#2108,.T.);
#3019=ORIENTED_EDGE('',*,*,#2294,.T.);
#3020=ORIENTED_EDGE('',*,*,#2231,.T.);
#3021=ORIENTED_EDGE('',*,*,#2216,.T.);
#3022=ORIENTED_EDGE('',*,*,#2084,.T.);
#3023=ORIENTED_EDGE('',*,*,#2295,.T.);
#3024=ORIENTED_EDGE('',*,*,#2222,.T.);
#3025=ORIENTED_EDGE('',*,*,#2201,.T.);
#3026=ORIENTED_EDGE('',*,*,#2104,.T.);
#3027=ORIENTED_EDGE('',*,*,#2296,.T.);
#3028=ORIENTED_EDGE('',*,*,#2225,.T.);
#3029=ORIENTED_EDGE('',*,*,#2204,.T.);
#3030=ORIENTED_EDGE('',*,*,#2100,.T.);
#3031=ORIENTED_EDGE('',*,*,#2297,.T.);
#3032=ORIENTED_EDGE('',*,*,#2270,.T.);
#3033=ORIENTED_EDGE('',*,*,#2207,.T.);
#3034=ORIENTED_EDGE('',*,*,#2096,.T.);
#3035=ORIENTED_EDGE('',*,*,#2298,.T.);
#3036=ORIENTED_EDGE('',*,*,#2264,.T.);
#3037=ORIENTED_EDGE('',*,*,#2210,.T.);
#3038=ORIENTED_EDGE('',*,*,#2092,.T.);
#3039=ORIENTED_EDGE('',*,*,#2299,.T.);
#3040=ORIENTED_EDGE('',*,*,#2261,.T.);
#3041=ORIENTED_EDGE('',*,*,#2213,.T.);
#3042=ORIENTED_EDGE('',*,*,#2088,.T.);
#3043=ORIENTED_EDGE('',*,*,#2300,.T.);
#3044=ORIENTED_EDGE('',*,*,#2252,.T.);
#3045=ORIENTED_EDGE('',*,*,#2160,.T.);
#3046=ORIENTED_EDGE('',*,*,#2277,.F.);
#3047=ORIENTED_EDGE('',*,*,#2143,.T.);
#3048=ORIENTED_EDGE('',*,*,#2301,.F.);
#3049=ORIENTED_EDGE('',*,*,#2302,.T.);
#3050=ORIENTED_EDGE('',*,*,#2282,.F.);
#3051=ORIENTED_EDGE('',*,*,#2091,.T.);
#3052=ORIENTED_EDGE('',*,*,#2303,.F.);
#3053=ORIENTED_EDGE('',*,*,#2253,.T.);
#3054=ORIENTED_EDGE('',*,*,#2300,.F.);
#3055=ORIENTED_EDGE('',*,*,#2250,.T.);
#3056=ORIENTED_EDGE('',*,*,#2278,.F.);
#3057=ORIENTED_EDGE('',*,*,#2159,.T.);
#3058=ORIENTED_EDGE('',*,*,#2304,.F.);
#3059=ORIENTED_EDGE('',*,*,#2241,.T.);
#3060=ORIENTED_EDGE('',*,*,#2279,.F.);
#3061=ORIENTED_EDGE('',*,*,#2155,.T.);
#3062=ORIENTED_EDGE('',*,*,#2305,.F.);
#3063=ORIENTED_EDGE('',*,*,#2238,.T.);
#3064=ORIENTED_EDGE('',*,*,#2280,.F.);
#3065=ORIENTED_EDGE('',*,*,#2151,.T.);
#3066=ORIENTED_EDGE('',*,*,#2306,.F.);
#3067=ORIENTED_EDGE('',*,*,#2229,.T.);
#3068=ORIENTED_EDGE('',*,*,#2281,.F.);
#3069=ORIENTED_EDGE('',*,*,#2147,.T.);
#3070=ORIENTED_EDGE('',*,*,#2307,.F.);
#3071=ORIENTED_EDGE('',*,*,#2220,.T.);
#3072=ORIENTED_EDGE('',*,*,#2286,.F.);
#3073=ORIENTED_EDGE('',*,*,#2308,.T.);
#3074=ORIENTED_EDGE('',*,*,#2309,.F.);
#3075=ORIENTED_EDGE('',*,*,#2274,.T.);
#3076=ORIENTED_EDGE('',*,*,#2287,.F.);
#3077=ORIENTED_EDGE('',*,*,#2139,.T.);
#3078=ORIENTED_EDGE('',*,*,#2310,.F.);
#3079=ORIENTED_EDGE('',*,*,#2268,.T.);
#3080=ORIENTED_EDGE('',*,*,#2288,.F.);
#3081=ORIENTED_EDGE('',*,*,#2135,.T.);
#3082=ORIENTED_EDGE('',*,*,#2311,.F.);
#3083=ORIENTED_EDGE('',*,*,#2259,.T.);
#3084=ORIENTED_EDGE('',*,*,#2289,.F.);
#3085=ORIENTED_EDGE('',*,*,#2131,.T.);
#3086=ORIENTED_EDGE('',*,*,#2312,.F.);
#3087=ORIENTED_EDGE('',*,*,#2256,.T.);
#3088=ORIENTED_EDGE('',*,*,#2290,.F.);
#3089=ORIENTED_EDGE('',*,*,#2127,.T.);
#3090=ORIENTED_EDGE('',*,*,#2313,.F.);
#3091=ORIENTED_EDGE('',*,*,#2247,.T.);
#3092=ORIENTED_EDGE('',*,*,#2291,.F.);
#3093=ORIENTED_EDGE('',*,*,#2123,.T.);
#3094=ORIENTED_EDGE('',*,*,#2314,.F.);
#3095=ORIENTED_EDGE('',*,*,#2244,.T.);
#3096=ORIENTED_EDGE('',*,*,#2292,.F.);
#3097=ORIENTED_EDGE('',*,*,#2119,.T.);
#3098=ORIENTED_EDGE('',*,*,#2315,.F.);
#3099=ORIENTED_EDGE('',*,*,#2235,.T.);
#3100=ORIENTED_EDGE('',*,*,#2293,.F.);
#3101=ORIENTED_EDGE('',*,*,#2115,.T.);
#3102=ORIENTED_EDGE('',*,*,#2316,.F.);
#3103=ORIENTED_EDGE('',*,*,#2087,.T.);
#3104=ORIENTED_EDGE('',*,*,#2317,.F.);
#3105=ORIENTED_EDGE('',*,*,#2223,.T.);
#3106=ORIENTED_EDGE('',*,*,#2295,.F.);
#3107=ORIENTED_EDGE('',*,*,#2226,.T.);
#3108=ORIENTED_EDGE('',*,*,#2296,.F.);
#3109=ORIENTED_EDGE('',*,*,#2107,.T.);
#3110=ORIENTED_EDGE('',*,*,#2318,.F.);
#3111=ORIENTED_EDGE('',*,*,#2271,.T.);
#3112=ORIENTED_EDGE('',*,*,#2297,.F.);
#3113=ORIENTED_EDGE('',*,*,#2103,.T.);
#3114=ORIENTED_EDGE('',*,*,#2319,.F.);
#3115=ORIENTED_EDGE('',*,*,#2265,.T.);
#3116=ORIENTED_EDGE('',*,*,#2298,.F.);
#3117=ORIENTED_EDGE('',*,*,#2099,.T.);
#3118=ORIENTED_EDGE('',*,*,#2320,.F.);
#3119=ORIENTED_EDGE('',*,*,#2262,.T.);
#3120=ORIENTED_EDGE('',*,*,#2299,.F.);
#3121=ORIENTED_EDGE('',*,*,#2095,.T.);
#3122=ORIENTED_EDGE('',*,*,#2321,.F.);
#3123=ORIENTED_EDGE('',*,*,#2285,.F.);
#3124=ORIENTED_EDGE('',*,*,#2322,.F.);
#3125=ORIENTED_EDGE('',*,*,#2323,.F.);
#3126=ORIENTED_EDGE('',*,*,#2308,.F.);
#3127=ORIENTED_EDGE('',*,*,#2284,.F.);
#3128=ORIENTED_EDGE('',*,*,#2324,.T.);
#3129=ORIENTED_EDGE('',*,*,#2325,.F.);
#3130=ORIENTED_EDGE('',*,*,#2322,.T.);
#3131=ORIENTED_EDGE('',*,*,#2283,.F.);
#3132=ORIENTED_EDGE('',*,*,#2302,.F.);
#3133=ORIENTED_EDGE('',*,*,#2326,.F.);
#3134=ORIENTED_EDGE('',*,*,#2324,.F.);
#3135=ORIENTED_EDGE('',*,*,#2327,.F.);
#3136=ORIENTED_EDGE('',*,*,#2328,.T.);
#3137=ORIENTED_EDGE('',*,*,#2162,.T.);
#3138=ORIENTED_EDGE('',*,*,#2254,.T.);
#3139=ORIENTED_EDGE('',*,*,#2303,.T.);
#3140=ORIENTED_EDGE('',*,*,#2090,.T.);
#3141=ORIENTED_EDGE('',*,*,#2215,.T.);
#3142=ORIENTED_EDGE('',*,*,#2263,.T.);
#3143=ORIENTED_EDGE('',*,*,#2321,.T.);
#3144=ORIENTED_EDGE('',*,*,#2094,.T.);
#3145=ORIENTED_EDGE('',*,*,#2212,.T.);
#3146=ORIENTED_EDGE('',*,*,#2266,.T.);
#3147=ORIENTED_EDGE('',*,*,#2320,.T.);
#3148=ORIENTED_EDGE('',*,*,#2098,.T.);
#3149=ORIENTED_EDGE('',*,*,#2209,.T.);
#3150=ORIENTED_EDGE('',*,*,#2272,.T.);
#3151=ORIENTED_EDGE('',*,*,#2319,.T.);
#3152=ORIENTED_EDGE('',*,*,#2102,.T.);
#3153=ORIENTED_EDGE('',*,*,#2206,.T.);
#3154=ORIENTED_EDGE('',*,*,#2227,.T.);
#3155=ORIENTED_EDGE('',*,*,#2318,.T.);
#3156=ORIENTED_EDGE('',*,*,#2106,.T.);
#3157=ORIENTED_EDGE('',*,*,#2203,.T.);
#3158=ORIENTED_EDGE('',*,*,#2224,.T.);
#3159=ORIENTED_EDGE('',*,*,#2317,.T.);
#3160=ORIENTED_EDGE('',*,*,#2086,.T.);
#3161=ORIENTED_EDGE('',*,*,#2218,.T.);
#3162=ORIENTED_EDGE('',*,*,#2233,.T.);
#3163=ORIENTED_EDGE('',*,*,#2329,.T.);
#3164=ORIENTED_EDGE('',*,*,#2110,.T.);
#3165=ORIENTED_EDGE('',*,*,#2200,.T.);
#3166=ORIENTED_EDGE('',*,*,#2236,.T.);
#3167=ORIENTED_EDGE('',*,*,#2316,.T.);
#3168=ORIENTED_EDGE('',*,*,#2114,.T.);
#3169=ORIENTED_EDGE('',*,*,#2197,.T.);
#3170=ORIENTED_EDGE('',*,*,#2245,.T.);
#3171=ORIENTED_EDGE('',*,*,#2315,.T.);
#3172=ORIENTED_EDGE('',*,*,#2118,.T.);
#3173=ORIENTED_EDGE('',*,*,#2194,.T.);
#3174=ORIENTED_EDGE('',*,*,#2248,.T.);
#3175=ORIENTED_EDGE('',*,*,#2314,.T.);
#3176=ORIENTED_EDGE('',*,*,#2122,.T.);
#3177=ORIENTED_EDGE('',*,*,#2191,.T.);
#3178=ORIENTED_EDGE('',*,*,#2257,.T.);
#3179=ORIENTED_EDGE('',*,*,#2313,.T.);
#3180=ORIENTED_EDGE('',*,*,#2126,.T.);
#3181=ORIENTED_EDGE('',*,*,#2188,.T.);
#3182=ORIENTED_EDGE('',*,*,#2260,.T.);
#3183=ORIENTED_EDGE('',*,*,#2312,.T.);
#3184=ORIENTED_EDGE('',*,*,#2130,.T.);
#3185=ORIENTED_EDGE('',*,*,#2185,.T.);
#3186=ORIENTED_EDGE('',*,*,#2269,.T.);
#3187=ORIENTED_EDGE('',*,*,#2311,.T.);
#3188=ORIENTED_EDGE('',*,*,#2134,.T.);
#3189=ORIENTED_EDGE('',*,*,#2182,.T.);
#3190=ORIENTED_EDGE('',*,*,#2275,.T.);
#3191=ORIENTED_EDGE('',*,*,#2310,.T.);
#3192=ORIENTED_EDGE('',*,*,#2138,.T.);
#3193=ORIENTED_EDGE('',*,*,#2179,.T.);
#3194=ORIENTED_EDGE('',*,*,#2221,.T.);
#3195=ORIENTED_EDGE('',*,*,#2309,.T.);
#3196=ORIENTED_EDGE('',*,*,#2323,.T.);
#3197=ORIENTED_EDGE('',*,*,#2325,.T.);
#3198=ORIENTED_EDGE('',*,*,#2326,.T.);
#3199=ORIENTED_EDGE('',*,*,#2301,.T.);
#3200=ORIENTED_EDGE('',*,*,#2142,.T.);
#3201=ORIENTED_EDGE('',*,*,#2176,.T.);
#3202=ORIENTED_EDGE('',*,*,#2230,.T.);
#3203=ORIENTED_EDGE('',*,*,#2307,.T.);
#3204=ORIENTED_EDGE('',*,*,#2146,.T.);
#3205=ORIENTED_EDGE('',*,*,#2173,.T.);
#3206=ORIENTED_EDGE('',*,*,#2239,.T.);
#3207=ORIENTED_EDGE('',*,*,#2306,.T.);
#3208=ORIENTED_EDGE('',*,*,#2150,.T.);
#3209=ORIENTED_EDGE('',*,*,#2170,.T.);
#3210=ORIENTED_EDGE('',*,*,#2242,.T.);
#3211=ORIENTED_EDGE('',*,*,#2305,.T.);
#3212=ORIENTED_EDGE('',*,*,#2154,.T.);
#3213=ORIENTED_EDGE('',*,*,#2167,.T.);
#3214=ORIENTED_EDGE('',*,*,#2251,.T.);
#3215=ORIENTED_EDGE('',*,*,#2304,.T.);
#3216=ORIENTED_EDGE('',*,*,#2158,.T.);
#3217=ORIENTED_EDGE('',*,*,#2163,.T.);
#3218=ORIENTED_EDGE('',*,*,#2328,.F.);
#3219=ORIENTED_EDGE('',*,*,#2081,.T.);
#3220=ORIENTED_EDGE('',*,*,#2327,.T.);
#3221=ORIENTED_EDGE('',*,*,#2276,.T.);
#3222=ORIENTED_EDGE('',*,*,#2232,.T.);
#3223=ORIENTED_EDGE('',*,*,#2294,.F.);
#3224=ORIENTED_EDGE('',*,*,#2111,.T.);
#3225=ORIENTED_EDGE('',*,*,#2329,.F.);
#3508=CYLINDRICAL_SURFACE('',#4049,0.75);
#3509=CYLINDRICAL_SURFACE('',#4149,25.);
#3510=CYLINDRICAL_SURFACE('',#4214,34.);
#3597=ADVANCED_FACE('',(#391),#3508,.F.);
#3598=ADVANCED_FACE('',(#392),#209,.T.);
#3599=ADVANCED_FACE('',(#393),#210,.F.);
#3600=ADVANCED_FACE('',(#394),#211,.F.);
#3601=ADVANCED_FACE('',(#395),#212,.F.);
#3602=ADVANCED_FACE('',(#396),#213,.F.);
#3603=ADVANCED_FACE('',(#397),#214,.F.);
#3604=ADVANCED_FACE('',(#398),#215,.F.);
#3605=ADVANCED_FACE('',(#399),#216,.F.);
#3606=ADVANCED_FACE('',(#400),#217,.F.);
#3607=ADVANCED_FACE('',(#401),#218,.F.);
#3608=ADVANCED_FACE('',(#402),#219,.F.);
#3609=ADVANCED_FACE('',(#403),#220,.F.);
#3610=ADVANCED_FACE('',(#404),#221,.F.);
#3611=ADVANCED_FACE('',(#405),#222,.F.);
#3612=ADVANCED_FACE('',(#406),#223,.F.);
#3613=ADVANCED_FACE('',(#407),#224,.F.);
#3614=ADVANCED_FACE('',(#408),#225,.F.);
#3615=ADVANCED_FACE('',(#409),#226,.F.);
#3616=ADVANCED_FACE('',(#410),#227,.F.);
#3617=ADVANCED_FACE('',(#411),#228,.F.);
#3618=ADVANCED_FACE('',(#412),#229,.T.);
#3619=ADVANCED_FACE('',(#413),#230,.T.);
#3620=ADVANCED_FACE('',(#414),#231,.T.);
#3621=ADVANCED_FACE('',(#415),#232,.T.);
#3622=ADVANCED_FACE('',(#416),#233,.T.);
#3623=ADVANCED_FACE('',(#417),#234,.T.);
#3624=ADVANCED_FACE('',(#418),#235,.T.);
#3625=ADVANCED_FACE('',(#419),#236,.T.);
#3626=ADVANCED_FACE('',(#420),#237,.T.);
#3627=ADVANCED_FACE('',(#421),#238,.T.);
#3628=ADVANCED_FACE('',(#422),#239,.T.);
#3629=ADVANCED_FACE('',(#423),#240,.T.);
#3630=ADVANCED_FACE('',(#424),#241,.T.);
#3631=ADVANCED_FACE('',(#425),#242,.T.);
#3632=ADVANCED_FACE('',(#426),#243,.T.);
#3633=ADVANCED_FACE('',(#427),#244,.T.);
#3634=ADVANCED_FACE('',(#428),#245,.T.);
#3635=ADVANCED_FACE('',(#429),#246,.T.);
#3636=ADVANCED_FACE('',(#430),#247,.T.);
#3637=ADVANCED_FACE('',(#431),#248,.F.);
#3638=ADVANCED_FACE('',(#432),#249,.F.);
#3639=ADVANCED_FACE('',(#433),#250,.F.);
#3640=ADVANCED_FACE('',(#434),#251,.F.);
#3641=ADVANCED_FACE('',(#435),#252,.F.);
#3642=ADVANCED_FACE('',(#436),#253,.F.);
#3643=ADVANCED_FACE('',(#437),#254,.F.);
#3644=ADVANCED_FACE('',(#438),#255,.F.);
#3645=ADVANCED_FACE('',(#439),#256,.F.);
#3646=ADVANCED_FACE('',(#440),#257,.F.);
#3647=ADVANCED_FACE('',(#441),#258,.F.);
#3648=ADVANCED_FACE('',(#442),#259,.F.);
#3649=ADVANCED_FACE('',(#443),#260,.F.);
#3650=ADVANCED_FACE('',(#444),#261,.F.);
#3651=ADVANCED_FACE('',(#445),#262,.F.);
#3652=ADVANCED_FACE('',(#446),#263,.F.);
#3653=ADVANCED_FACE('',(#447),#264,.F.);
#3654=ADVANCED_FACE('',(#448),#265,.F.);
#3655=ADVANCED_FACE('',(#449),#266,.F.);
#3656=ADVANCED_FACE('',(#450),#3509,.F.);
#3657=ADVANCED_FACE('',(#451),#267,.F.);
#3658=ADVANCED_FACE('',(#452),#268,.F.);
#3659=ADVANCED_FACE('',(#453),#269,.F.);
#3660=ADVANCED_FACE('',(#454),#270,.F.);
#3661=ADVANCED_FACE('',(#455),#271,.F.);
#3662=ADVANCED_FACE('',(#456),#272,.F.);
#3663=ADVANCED_FACE('',(#457),#273,.F.);
#3664=ADVANCED_FACE('',(#458),#274,.F.);
#3665=ADVANCED_FACE('',(#459),#275,.F.);
#3666=ADVANCED_FACE('',(#460),#276,.F.);
#3667=ADVANCED_FACE('',(#461),#277,.F.);
#3668=ADVANCED_FACE('',(#462),#278,.F.);
#3669=ADVANCED_FACE('',(#463),#279,.F.);
#3670=ADVANCED_FACE('',(#464),#280,.F.);
#3671=ADVANCED_FACE('',(#465),#281,.F.);
#3672=ADVANCED_FACE('',(#466),#282,.F.);
#3673=ADVANCED_FACE('',(#467),#283,.F.);
#3674=ADVANCED_FACE('',(#468),#284,.F.);
#3675=ADVANCED_FACE('',(#469),#285,.F.);
#3676=ADVANCED_FACE('',(#470),#286,.F.);
#3677=ADVANCED_FACE('',(#471),#287,.T.);
#3678=ADVANCED_FACE('',(#472),#288,.F.);
#3679=ADVANCED_FACE('',(#473,#170),#3510,.T.);
#3680=ADVANCED_FACE('',(#474,#171),#289,.T.);
#3681=ADVANCED_FACE('',(#475),#290,.F.);
#3757=CLOSED_SHELL('',(#3597,#3598,#3599,#3600,#3601,#3602,#3603,#3604,
#3605,#3606,#3607,#3608,#3609,#3610,#3611,#3612,#3613,#3614,#3615,#3616,
#3617,#3618,#3619,#3620,#3621,#3622,#3623,#3624,#3625,#3626,#3627,#3628,
#3629,#3630,#3631,#3632,#3633,#3634,#3635,#3636,#3637,#3638,#3639,#3640,
#3641,#3642,#3643,#3644,#3645,#3646,#3647,#3648,#3649,#3650,#3651,#3652,
#3653,#3654,#3655,#3656,#3657,#3658,#3659,#3660,#3661,#3662,#3663,#3664,
#3665,#3666,#3667,#3668,#3669,#3670,#3671,#3672,#3673,#3674,#3675,#3676,
#3677,#3678,#3679,#3680,#3681));
#4048=AXIS2_PLACEMENT_3D('',#5890,#4696,#4697);
#4049=AXIS2_PLACEMENT_3D('',#5891,#4698,#4699);
#4050=AXIS2_PLACEMENT_3D('',#5929,#4701,#4702);
#4051=AXIS2_PLACEMENT_3D('',#5930,#4703,#4704);
#4052=AXIS2_PLACEMENT_3D('',#5931,#4705,#4706);
#4053=AXIS2_PLACEMENT_3D('',#5940,#4711,#4712);
#4054=AXIS2_PLACEMENT_3D('',#5949,#4717,#4718);
#4055=AXIS2_PLACEMENT_3D('',#5958,#4723,#4724);
#4056=AXIS2_PLACEMENT_3D('',#5967,#4729,#4730);
#4057=AXIS2_PLACEMENT_3D('',#5976,#4735,#4736);
#4058=AXIS2_PLACEMENT_3D('',#5985,#4741,#4742);
#4059=AXIS2_PLACEMENT_3D('',#5994,#4747,#4748);
#4060=AXIS2_PLACEMENT_3D('',#6003,#4753,#4754);
#4061=AXIS2_PLACEMENT_3D('',#6012,#4759,#4760);
#4062=AXIS2_PLACEMENT_3D('',#6021,#4765,#4766);
#4063=AXIS2_PLACEMENT_3D('',#6030,#4771,#4772);
#4064=AXIS2_PLACEMENT_3D('',#6039,#4777,#4778);
#4065=AXIS2_PLACEMENT_3D('',#6048,#4783,#4784);
#4066=AXIS2_PLACEMENT_3D('',#6057,#4789,#4790);
#4067=AXIS2_PLACEMENT_3D('',#6066,#4795,#4796);
#4068=AXIS2_PLACEMENT_3D('',#6075,#4801,#4802);
#4069=AXIS2_PLACEMENT_3D('',#6084,#4807,#4808);
#4070=AXIS2_PLACEMENT_3D('',#6093,#4813,#4814);
#4071=AXIS2_PLACEMENT_3D('',#6102,#4819,#4820);
#4072=AXIS2_PLACEMENT_3D('',#6105,#4821,#4822);
#4073=AXIS2_PLACEMENT_3D('',#6109,#4824,#4825);
#4074=AXIS2_PLACEMENT_3D('',#6110,#4826,#4827);
#4075=AXIS2_PLACEMENT_3D('',#6111,#4828,#4829);
#4076=AXIS2_PLACEMENT_3D('',#6112,#4830,#4831);
#4077=AXIS2_PLACEMENT_3D('',#6114,#4832,#4833);
#4078=AXIS2_PLACEMENT_3D('',#6117,#4835,#4836);
#4079=AXIS2_PLACEMENT_3D('',#6118,#4837,#4838);
#4080=AXIS2_PLACEMENT_3D('',#6120,#4839,#4840);
#4081=AXIS2_PLACEMENT_3D('',#6123,#4842,#4843);
#4082=AXIS2_PLACEMENT_3D('',#6124,#4844,#4845);
#4083=AXIS2_PLACEMENT_3D('',#6126,#4846,#4847);
#4084=AXIS2_PLACEMENT_3D('',#6129,#4849,#4850);
#4085=AXIS2_PLACEMENT_3D('',#6130,#4851,#4852);
#4086=AXIS2_PLACEMENT_3D('',#6132,#4853,#4854);
#4087=AXIS2_PLACEMENT_3D('',#6135,#4856,#4857);
#4088=AXIS2_PLACEMENT_3D('',#6136,#4858,#4859);
#4089=AXIS2_PLACEMENT_3D('',#6138,#4860,#4861);
#4090=AXIS2_PLACEMENT_3D('',#6141,#4863,#4864);
#4091=AXIS2_PLACEMENT_3D('',#6142,#4865,#4866);
#4092=AXIS2_PLACEMENT_3D('',#6144,#4867,#4868);
#4093=AXIS2_PLACEMENT_3D('',#6147,#4870,#4871);
#4094=AXIS2_PLACEMENT_3D('',#6148,#4872,#4873);
#4095=AXIS2_PLACEMENT_3D('',#6150,#4874,#4875);
#4096=AXIS2_PLACEMENT_3D('',#6153,#4877,#4878);
#4097=AXIS2_PLACEMENT_3D('',#6154,#4879,#4880);
#4098=AXIS2_PLACEMENT_3D('',#6156,#4881,#4882);
#4099=AXIS2_PLACEMENT_3D('',#6159,#4884,#4885);
#4100=AXIS2_PLACEMENT_3D('',#6160,#4886,#4887);
#4101=AXIS2_PLACEMENT_3D('',#6162,#4888,#4889);
#4102=AXIS2_PLACEMENT_3D('',#6165,#4891,#4892);
#4103=AXIS2_PLACEMENT_3D('',#6166,#4893,#4894);
#4104=AXIS2_PLACEMENT_3D('',#6168,#4895,#4896);
#4105=AXIS2_PLACEMENT_3D('',#6171,#4898,#4899);
#4106=AXIS2_PLACEMENT_3D('',#6172,#4900,#4901);
#4107=AXIS2_PLACEMENT_3D('',#6174,#4902,#4903);
#4108=AXIS2_PLACEMENT_3D('',#6177,#4905,#4906);
#4109=AXIS2_PLACEMENT_3D('',#6178,#4907,#4908);
#4110=AXIS2_PLACEMENT_3D('',#6180,#4909,#4910);
#4111=AXIS2_PLACEMENT_3D('',#6183,#4912,#4913);
#4112=AXIS2_PLACEMENT_3D('',#6184,#4914,#4915);
#4113=AXIS2_PLACEMENT_3D('',#6186,#4916,#4917);
#4114=AXIS2_PLACEMENT_3D('',#6189,#4919,#4920);
#4115=AXIS2_PLACEMENT_3D('',#6190,#4921,#4922);
#4116=AXIS2_PLACEMENT_3D('',#6192,#4923,#4924);
#4117=AXIS2_PLACEMENT_3D('',#6195,#4926,#4927);
#4118=AXIS2_PLACEMENT_3D('',#6196,#4928,#4929);
#4119=AXIS2_PLACEMENT_3D('',#6198,#4930,#4931);
#4120=AXIS2_PLACEMENT_3D('',#6201,#4933,#4934);
#4121=AXIS2_PLACEMENT_3D('',#6202,#4935,#4936);
#4122=AXIS2_PLACEMENT_3D('',#6204,#4937,#4938);
#4123=AXIS2_PLACEMENT_3D('',#6207,#4940,#4941);
#4124=AXIS2_PLACEMENT_3D('',#6208,#4942,#4943);
#4125=AXIS2_PLACEMENT_3D('',#6210,#4944,#4945);
#4126=AXIS2_PLACEMENT_3D('',#6213,#4947,#4948);
#4127=AXIS2_PLACEMENT_3D('',#6214,#4949,#4950);
#4128=AXIS2_PLACEMENT_3D('',#6216,#4951,#4952);
#4129=AXIS2_PLACEMENT_3D('',#6219,#4954,#4955);
#4130=AXIS2_PLACEMENT_3D('',#6220,#4956,#4957);
#4131=AXIS2_PLACEMENT_3D('',#6226,#4961,#4962);
#4132=AXIS2_PLACEMENT_3D('',#6232,#4966,#4967);
#4133=AXIS2_PLACEMENT_3D('',#6238,#4971,#4972);
#4134=AXIS2_PLACEMENT_3D('',#6244,#4976,#4977);
#4135=AXIS2_PLACEMENT_3D('',#6250,#4981,#4982);
#4136=AXIS2_PLACEMENT_3D('',#6256,#4986,#4987);
#4137=AXIS2_PLACEMENT_3D('',#6262,#4991,#4992);
#4138=AXIS2_PLACEMENT_3D('',#6268,#4996,#4997);
#4139=AXIS2_PLACEMENT_3D('',#6274,#5001,#5002);
#4140=AXIS2_PLACEMENT_3D('',#6280,#5006,#5007);
#4141=AXIS2_PLACEMENT_3D('',#6286,#5011,#5012);
#4142=AXIS2_PLACEMENT_3D('',#6292,#5016,#5017);
#4143=AXIS2_PLACEMENT_3D('',#6298,#5021,#5022);
#4144=AXIS2_PLACEMENT_3D('',#6304,#5026,#5027);
#4145=AXIS2_PLACEMENT_3D('',#6310,#5031,#5032);
#4146=AXIS2_PLACEMENT_3D('',#6316,#5036,#5037);
#4147=AXIS2_PLACEMENT_3D('',#6322,#5041,#5042);
#4148=AXIS2_PLACEMENT_3D('',#6328,#5046,#5047);
#4149=AXIS2_PLACEMENT_3D('',#6334,#5051,#5052);
#4150=AXIS2_PLACEMENT_3D('',#6336,#5053,#5054);
#4151=AXIS2_PLACEMENT_3D('',#6338,#5056,#5057);
#4152=AXIS2_PLACEMENT_3D('',#6339,#5058,#5059);
#4153=AXIS2_PLACEMENT_3D('',#6340,#5060,#5061);
#4154=AXIS2_PLACEMENT_3D('',#6341,#5062,#5063);
#4155=AXIS2_PLACEMENT_3D('',#6343,#5064,#5065);
#4156=AXIS2_PLACEMENT_3D('',#6347,#5067,#5068);
#4157=AXIS2_PLACEMENT_3D('',#6350,#5070,#5071);
#4158=AXIS2_PLACEMENT_3D('',#6351,#5072,#5073);
#4159=AXIS2_PLACEMENT_3D('',#6352,#5074,#5075);
#4160=AXIS2_PLACEMENT_3D('',#6353,#5076,#5077);
#4161=AXIS2_PLACEMENT_3D('',#6354,#5078,#5079);
#4162=AXIS2_PLACEMENT_3D('',#6355,#5080,#5081);
#4163=AXIS2_PLACEMENT_3D('',#6356,#5082,#5083);
#4164=AXIS2_PLACEMENT_3D('',#6357,#5084,#5085);
#4165=AXIS2_PLACEMENT_3D('',#6358,#5086,#5087);
#4166=AXIS2_PLACEMENT_3D('',#6359,#5088,#5089);
#4167=AXIS2_PLACEMENT_3D('',#6360,#5090,#5091);
#4168=AXIS2_PLACEMENT_3D('',#6361,#5092,#5093);
#4169=AXIS2_PLACEMENT_3D('',#6362,#5094,#5095);
#4170=AXIS2_PLACEMENT_3D('',#6363,#5096,#5097);
#4171=AXIS2_PLACEMENT_3D('',#6364,#5098,#5099);
#4172=AXIS2_PLACEMENT_3D('',#6365,#5100,#5101);
#4173=AXIS2_PLACEMENT_3D('',#6367,#5102,#5103);
#4174=AXIS2_PLACEMENT_3D('',#6369,#5105,#5106);
#4175=AXIS2_PLACEMENT_3D('',#6370,#5107,#5108);
#4176=AXIS2_PLACEMENT_3D('',#6371,#5109,#5110);
#4177=AXIS2_PLACEMENT_3D('',#6372,#5111,#5112);
#4178=AXIS2_PLACEMENT_3D('',#6373,#5113,#5114);
#4179=AXIS2_PLACEMENT_3D('',#6374,#5115,#5116);
#4180=AXIS2_PLACEMENT_3D('',#6375,#5117,#5118);
#4181=AXIS2_PLACEMENT_3D('',#6376,#5119,#5120);
#4182=AXIS2_PLACEMENT_3D('',#6377,#5121,#5122);
#4183=AXIS2_PLACEMENT_3D('',#6378,#5123,#5124);
#4184=AXIS2_PLACEMENT_3D('',#6379,#5125,#5126);
#4185=AXIS2_PLACEMENT_3D('',#6382,#5128,#5129);
#4186=AXIS2_PLACEMENT_3D('',#6383,#5130,#5131);
#4187=AXIS2_PLACEMENT_3D('',#6384,#5132,#5133);
#4188=AXIS2_PLACEMENT_3D('',#6385,#5134,#5135);
#4189=AXIS2_PLACEMENT_3D('',#6386,#5136,#5137);
#4190=AXIS2_PLACEMENT_3D('',#6387,#5138,#5139);
#4191=AXIS2_PLACEMENT_3D('',#6388,#5140,#5141);
#4192=AXIS2_PLACEMENT_3D('',#6389,#5142,#5143);
#4193=AXIS2_PLACEMENT_3D('',#6390,#5144,#5145);
#4194=AXIS2_PLACEMENT_3D('',#6391,#5146,#5147);
#4195=AXIS2_PLACEMENT_3D('',#6392,#5148,#5149);
#4196=AXIS2_PLACEMENT_3D('',#6393,#5150,#5151);
#4197=AXIS2_PLACEMENT_3D('',#6394,#5152,#5153);
#4198=AXIS2_PLACEMENT_3D('',#6395,#5154,#5155);
#4199=AXIS2_PLACEMENT_3D('',#6396,#5156,#5157);
#4200=AXIS2_PLACEMENT_3D('',#6397,#5158,#5159);
#4201=AXIS2_PLACEMENT_3D('',#6398,#5160,#5161);
#4202=AXIS2_PLACEMENT_3D('',#6399,#5162,#5163);
#4203=AXIS2_PLACEMENT_3D('',#6400,#5164,#5165);
#4204=AXIS2_PLACEMENT_3D('',#6401,#5166,#5167);
#4205=AXIS2_PLACEMENT_3D('',#6402,#5168,#5169);
#4206=AXIS2_PLACEMENT_3D('',#6403,#5170,#5171);
#4207=AXIS2_PLACEMENT_3D('',#6404,#5172,#5173);
#4208=AXIS2_PLACEMENT_3D('',#6405,#5174,#5175);
#4209=AXIS2_PLACEMENT_3D('',#6406,#5176,#5177);
#4210=AXIS2_PLACEMENT_3D('',#6407,#5178,#5179);
#4211=AXIS2_PLACEMENT_3D('',#6411,#5182,#5183);
#4212=AXIS2_PLACEMENT_3D('',#6414,#5185,#5186);
#4213=AXIS2_PLACEMENT_3D('',#6415,#5187,#5188);
#4214=AXIS2_PLACEMENT_3D('',#6417,#5190,#5191);
#4215=AXIS2_PLACEMENT_3D('',#6419,#5192,#5193);
#4216=AXIS2_PLACEMENT_3D('',#6421,#5195,#5196);
#4217=AXIS2_PLACEMENT_3D('',#6422,#5197,#5198);
#4218=AXIS2_PLACEMENT_3D('',#6423,#5199,#5200);
#4696=DIRECTION('axis',(0.,0.,1.));
#4697=DIRECTION('refdir',(1.,0.,0.));
#4698=DIRECTION('center_axis',(0.,0.,-1.));
#4699=DIRECTION('ref_axis',(1.,0.,0.));
#4700=DIRECTION('',(0.,0.,-1.));
#4701=DIRECTION('center_axis',(0.,0.,-1.));
#4702=DIRECTION('ref_axis',(1.,0.,0.));
#4703=DIRECTION('center_axis',(0.,0.,1.));
#4704=DIRECTION('ref_axis',(1.,0.,0.));
#4705=DIRECTION('center_axis',(-0.951056516295154,0.,0.309016994374948));
#4706=DIRECTION('ref_axis',(-0.309016994374948,0.,-0.951056516295154));
#4707=DIRECTION('',(0.,-1.,0.));
#4708=DIRECTION('',(-0.309016994374948,0.,-0.951056516295154));
#4709=DIRECTION('',(0.,1.,0.));
#4710=DIRECTION('',(0.309016994374948,0.,0.951056516295154));
#4711=DIRECTION('center_axis',(-0.309016994374948,0.,-0.951056516295154));
#4712=DIRECTION('ref_axis',(0.951056516295154,0.,-0.309016994374948));
#4713=DIRECTION('',(0.,-1.,0.));
#4714=DIRECTION('',(0.951056516295154,0.,-0.309016994374948));
#4715=DIRECTION('',(0.,1.,0.));
#4716=DIRECTION('',(-0.951056516295154,0.,0.309016994374948));
#4717=DIRECTION('center_axis',(-0.587785252292473,0.,-0.809016994374947));
#4718=DIRECTION('ref_axis',(0.809016994374947,0.,-0.587785252292473));
#4719=DIRECTION('',(0.,-1.,0.));
#4720=DIRECTION('',(0.809016994374947,0.,-0.587785252292473));
#4721=DIRECTION('',(0.,1.,0.));
#4722=DIRECTION('',(-0.809016994374947,0.,0.587785252292473));
#4723=DIRECTION('center_axis',(-0.809016994374948,0.,-0.587785252292473));
#4724=DIRECTION('ref_axis',(0.587785252292473,0.,-0.809016994374947));
#4725=DIRECTION('',(0.,-1.,0.));
#4726=DIRECTION('',(0.587785252292473,0.,-0.809016994374947));
#4727=DIRECTION('',(0.,1.,0.));
#4728=DIRECTION('',(-0.587785252292473,0.,0.809016994374947));
#4729=DIRECTION('center_axis',(-0.951056516295154,0.,-0.309016994374947));
#4730=DIRECTION('ref_axis',(0.309016994374947,0.,-0.951056516295154));
#4731=DIRECTION('',(0.,-1.,0.));
#4732=DIRECTION('',(0.309016994374947,0.,-0.951056516295154));
#4733=DIRECTION('',(0.,1.,0.));
#4734=DIRECTION('',(-0.309016994374947,0.,0.951056516295154));
#4735=DIRECTION('center_axis',(-1.,0.,1.11022302462516E-16));
#4736=DIRECTION('ref_axis',(-1.11022302462516E-16,0.,-1.));
#4737=DIRECTION('',(0.,-1.,0.));
#4738=DIRECTION('',(-1.11022302462516E-16,0.,-1.));
#4739=DIRECTION('',(0.,1.,0.));
#4740=DIRECTION('',(1.11022302462516E-16,0.,1.));
#4741=DIRECTION('center_axis',(-0.809016994374947,0.,0.587785252292473));
#4742=DIRECTION('ref_axis',(-0.587785252292473,0.,-0.809016994374947));
#4743=DIRECTION('',(0.,-1.,0.));
#4744=DIRECTION('',(-0.587785252292473,0.,-0.809016994374947));
#4745=DIRECTION('',(0.,1.,0.));
#4746=DIRECTION('',(0.587785252292473,0.,0.809016994374947));
#4747=DIRECTION('center_axis',(-0.587785252292473,0.,0.809016994374947));
#4748=DIRECTION('ref_axis',(-0.809016994374947,0.,-0.587785252292473));
#4749=DIRECTION('',(0.,-1.,0.));
#4750=DIRECTION('',(-0.809016994374947,0.,-0.587785252292473));
#4751=DIRECTION('',(0.,1.,0.));
#4752=DIRECTION('',(0.809016994374947,0.,0.587785252292473));
#4753=DIRECTION('center_axis',(-0.309016994374947,0.,0.951056516295154));
#4754=DIRECTION('ref_axis',(-0.951056516295154,0.,-0.309016994374947));
#4755=DIRECTION('',(0.,-1.,0.));
#4756=DIRECTION('',(-0.951056516295154,0.,-0.309016994374947));
#4757=DIRECTION('',(0.,1.,0.));
#4758=DIRECTION('',(0.951056516295154,0.,0.309016994374947));
#4759=DIRECTION('center_axis',(5.55111512312578E-17,0.,1.));
#4760=DIRECTION('ref_axis',(-1.,0.,5.55111512312578E-17));
#4761=DIRECTION('',(0.,-1.,0.));
#4762=DIRECTION('',(-1.,0.,5.55111512312578E-17));
#4763=DIRECTION('',(0.,1.,0.));
#4764=DIRECTION('',(1.,0.,-5.55111512312578E-17));
#4765=DIRECTION('center_axis',(0.309016994374948,0.,0.951056516295154));
#4766=DIRECTION('ref_axis',(-0.951056516295154,0.,0.309016994374948));
#4767=DIRECTION('',(0.,-1.,0.));
#4768=DIRECTION('',(-0.951056516295154,0.,0.309016994374948));
#4769=DIRECTION('',(0.,1.,0.));
#4770=DIRECTION('',(0.951056516295154,0.,-0.309016994374948));
#4771=DIRECTION('center_axis',(0.587785252292473,0.,0.809016994374947));
#4772=DIRECTION('ref_axis',(-0.809016994374947,0.,0.587785252292473));
#4773=DIRECTION('',(0.,-1.,0.));
#4774=DIRECTION('',(-0.809016994374947,0.,0.587785252292473));
#4775=DIRECTION('',(0.,1.,0.));
#4776=DIRECTION('',(0.809016994374947,0.,-0.587785252292473));
#4777=DIRECTION('center_axis',(0.809016994374948,0.,0.587785252292473));
#4778=DIRECTION('ref_axis',(-0.587785252292473,0.,0.809016994374947));
#4779=DIRECTION('',(0.,-1.,0.));
#4780=DIRECTION('',(-0.587785252292473,0.,0.809016994374947));
#4781=DIRECTION('',(0.,1.,0.));
#4782=DIRECTION('',(0.587785252292473,0.,-0.809016994374947));
#4783=DIRECTION('center_axis',(0.951056516295154,0.,0.309016994374947));
#4784=DIRECTION('ref_axis',(-0.309016994374947,0.,0.951056516295154));
#4785=DIRECTION('',(0.,-1.,0.));
#4786=DIRECTION('',(-0.309016994374947,0.,0.951056516295154));
#4787=DIRECTION('',(0.,1.,0.));
#4788=DIRECTION('',(0.309016994374947,0.,-0.951056516295154));
#4789=DIRECTION('center_axis',(0.951056516295154,0.,-0.309016994374948));
#4790=DIRECTION('ref_axis',(0.309016994374948,0.,0.951056516295154));
#4791=DIRECTION('',(0.,-1.,0.));
#4792=DIRECTION('',(0.309016994374948,0.,0.951056516295154));
#4793=DIRECTION('',(0.,1.,0.));
#4794=DIRECTION('',(-0.309016994374948,0.,-0.951056516295154));
#4795=DIRECTION('center_axis',(0.809016994374947,0.,-0.587785252292473));
#4796=DIRECTION('ref_axis',(0.587785252292473,0.,0.809016994374947));
#4797=DIRECTION('',(0.,-1.,0.));
#4798=DIRECTION('',(0.587785252292473,0.,0.809016994374947));
#4799=DIRECTION('',(0.,1.,0.));
#4800=DIRECTION('',(-0.587785252292473,0.,-0.809016994374947));
#4801=DIRECTION('center_axis',(0.587785252292473,0.,-0.809016994374947));
#4802=DIRECTION('ref_axis',(0.809016994374947,0.,0.587785252292473));
#4803=DIRECTION('',(0.,-1.,0.));
#4804=DIRECTION('',(0.809016994374947,0.,0.587785252292473));
#4805=DIRECTION('',(0.,1.,0.));
#4806=DIRECTION('',(-0.809016994374947,0.,-0.587785252292473));
#4807=DIRECTION('center_axis',(0.309016994374947,0.,-0.951056516295154));
#4808=DIRECTION('ref_axis',(0.951056516295154,0.,0.309016994374947));
#4809=DIRECTION('',(0.,-1.,0.));
#4810=DIRECTION('',(0.951056516295154,0.,0.309016994374947));
#4811=DIRECTION('',(0.,1.,0.));
#4812=DIRECTION('',(-0.951056516295154,0.,-0.309016994374947));
#4813=DIRECTION('center_axis',(-1.11022302462516E-16,0.,-1.));
#4814=DIRECTION('ref_axis',(1.,0.,-1.11022302462516E-16));
#4815=DIRECTION('',(0.,-1.,0.));
#4816=DIRECTION('',(1.,0.,-1.11022302462516E-16));
#4817=DIRECTION('',(0.,1.,0.));
#4818=DIRECTION('',(-1.,0.,1.11022302462516E-16));
#4819=DIRECTION('center_axis',(0.,-1.,0.));
#4820=DIRECTION('ref_axis',(0.309016994374947,0.,-0.951056516295154));
#4821=DIRECTION('center_axis',(0.,-1.,0.));
#4822=DIRECTION('ref_axis',(1.,0.,0.));
#4823=DIRECTION('',(-1.,0.,2.77555756156289E-16));
#4824=DIRECTION('center_axis',(0.,1.,0.));
#4825=DIRECTION('ref_axis',(1.,0.,0.));
#4826=DIRECTION('center_axis',(0.,1.,0.));
#4827=DIRECTION('ref_axis',(1.,0.,0.));
#4828=DIRECTION('center_axis',(0.,-1.,0.));
#4829=DIRECTION('ref_axis',(1.,0.,0.));
#4830=DIRECTION('center_axis',(0.,-1.,0.));
#4831=DIRECTION('ref_axis',(0.309016994374947,0.,-0.951056516295154));
#4832=DIRECTION('center_axis',(0.,-1.,0.));
#4833=DIRECTION('ref_axis',(1.,0.,0.));
#4834=DIRECTION('',(-0.951056516295154,0.,-0.309016994374947));
#4835=DIRECTION('center_axis',(0.,1.,0.));
#4836=DIRECTION('ref_axis',(1.,0.,0.));
#4837=DIRECTION('center_axis',(0.,-1.,0.));
#4838=DIRECTION('ref_axis',(0.309016994374947,0.,-0.951056516295154));
#4839=DIRECTION('center_axis',(0.,-1.,0.));
#4840=DIRECTION('ref_axis',(1.,0.,0.));
#4841=DIRECTION('',(-0.809016994374948,0.,-0.587785252292473));
#4842=DIRECTION('center_axis',(0.,1.,0.));
#4843=DIRECTION('ref_axis',(1.,0.,0.));
#4844=DIRECTION('center_axis',(0.,-1.,0.));
#4845=DIRECTION('ref_axis',(0.309016994374947,0.,-0.951056516295154));
#4846=DIRECTION('center_axis',(0.,-1.,0.));
#4847=DIRECTION('ref_axis',(1.,0.,0.));
#4848=DIRECTION('',(-0.587785252292473,0.,-0.809016994374947));
#4849=DIRECTION('center_axis',(0.,1.,0.));
#4850=DIRECTION('ref_axis',(1.,0.,0.));
#4851=DIRECTION('center_axis',(0.,-1.,0.));
#4852=DIRECTION('ref_axis',(0.309016994374947,0.,-0.951056516295154));
#4853=DIRECTION('center_axis',(0.,-1.,0.));
#4854=DIRECTION('ref_axis',(1.,0.,0.));
#4855=DIRECTION('',(-0.309016994374948,0.,-0.951056516295153));
#4856=DIRECTION('center_axis',(0.,1.,0.));
#4857=DIRECTION('ref_axis',(1.,0.,0.));
#4858=DIRECTION('center_axis',(0.,-1.,0.));
#4859=DIRECTION('ref_axis',(0.309016994374947,0.,-0.951056516295154));
#4860=DIRECTION('center_axis',(0.,-1.,0.));
#4861=DIRECTION('ref_axis',(1.,0.,0.));
#4862=DIRECTION('',(0.309016994374947,0.,-0.951056516295154));
#4863=DIRECTION('center_axis',(0.,1.,0.));
#4864=DIRECTION('ref_axis',(1.,0.,0.));
#4865=DIRECTION('center_axis',(0.,-1.,0.));
#4866=DIRECTION('ref_axis',(0.309016994374947,0.,-0.951056516295154));
#4867=DIRECTION('center_axis',(0.,-1.,0.));
#4868=DIRECTION('ref_axis',(1.,0.,0.));
#4869=DIRECTION('',(0.587785252292473,0.,-0.809016994374947));
#4870=DIRECTION('center_axis',(0.,1.,0.));
#4871=DIRECTION('ref_axis',(1.,0.,0.));
#4872=DIRECTION('center_axis',(0.,-1.,0.));
#4873=DIRECTION('ref_axis',(0.309016994374947,0.,-0.951056516295154));
#4874=DIRECTION('center_axis',(0.,-1.,0.));
#4875=DIRECTION('ref_axis',(1.,0.,0.));
#4876=DIRECTION('',(0.809016994374947,0.,-0.587785252292473));
#4877=DIRECTION('center_axis',(0.,1.,0.));
#4878=DIRECTION('ref_axis',(1.,0.,0.));
#4879=DIRECTION('center_axis',(0.,-1.,0.));
#4880=DIRECTION('ref_axis',(0.309016994374947,0.,-0.951056516295154));
#4881=DIRECTION('center_axis',(0.,-1.,0.));
#4882=DIRECTION('ref_axis',(1.,0.,0.));
#4883=DIRECTION('',(0.951056516295154,0.,-0.309016994374948));
#4884=DIRECTION('center_axis',(0.,1.,0.));
#4885=DIRECTION('ref_axis',(1.,0.,0.));
#4886=DIRECTION('center_axis',(0.,-1.,0.));
#4887=DIRECTION('ref_axis',(0.309016994374947,0.,-0.951056516295154));
#4888=DIRECTION('center_axis',(0.,-1.,0.));
#4889=DIRECTION('ref_axis',(1.,0.,0.));
#4890=DIRECTION('',(1.,0.,-1.11022302462516E-16));
#4891=DIRECTION('center_axis',(0.,1.,0.));
#4892=DIRECTION('ref_axis',(1.,0.,0.));
#4893=DIRECTION('center_axis',(0.,-1.,0.));
#4894=DIRECTION('ref_axis',(0.309016994374947,0.,-0.951056516295154));
#4895=DIRECTION('center_axis',(0.,-1.,0.));
#4896=DIRECTION('ref_axis',(1.,0.,0.));
#4897=DIRECTION('',(0.951056516295154,0.,0.309016994374947));
#4898=DIRECTION('center_axis',(0.,1.,0.));
#4899=DIRECTION('ref_axis',(1.,0.,0.));
#4900=DIRECTION('center_axis',(0.,-1.,0.));
#4901=DIRECTION('ref_axis',(0.309016994374947,0.,-0.951056516295154));
#4902=DIRECTION('center_axis',(0.,-1.,0.));
#4903=DIRECTION('ref_axis',(1.,0.,0.));
#4904=DIRECTION('',(0.809016994374947,0.,0.587785252292473));
#4905=DIRECTION('center_axis',(0.,1.,0.));
#4906=DIRECTION('ref_axis',(1.,0.,0.));
#4907=DIRECTION('center_axis',(0.,-1.,0.));
#4908=DIRECTION('ref_axis',(0.309016994374947,0.,-0.951056516295154));
#4909=DIRECTION('center_axis',(0.,-1.,0.));
#4910=DIRECTION('ref_axis',(1.,0.,0.));
#4911=DIRECTION('',(0.587785252292473,0.,0.809016994374947));
#4912=DIRECTION('center_axis',(0.,1.,0.));
#4913=DIRECTION('ref_axis',(1.,0.,0.));
#4914=DIRECTION('center_axis',(0.,-1.,0.));
#4915=DIRECTION('ref_axis',(0.309016994374947,0.,-0.951056516295154));
#4916=DIRECTION('center_axis',(0.,-1.,0.));
#4917=DIRECTION('ref_axis',(1.,0.,0.));
#4918=DIRECTION('',(1.66533453693773E-16,0.,1.));
#4919=DIRECTION('center_axis',(0.,1.,0.));
#4920=DIRECTION('ref_axis',(1.,0.,0.));
#4921=DIRECTION('center_axis',(0.,-1.,0.));
#4922=DIRECTION('ref_axis',(0.309016994374947,0.,-0.951056516295154));
#4923=DIRECTION('center_axis',(0.,-1.,0.));
#4924=DIRECTION('ref_axis',(1.,0.,0.));
#4925=DIRECTION('',(-0.309016994374947,0.,0.951056516295154));
#4926=DIRECTION('center_axis',(0.,1.,0.));
#4927=DIRECTION('ref_axis',(1.,0.,0.));
#4928=DIRECTION('center_axis',(0.,-1.,0.));
#4929=DIRECTION('ref_axis',(0.309016994374947,0.,-0.951056516295154));
#4930=DIRECTION('center_axis',(0.,-1.,0.));
#4931=DIRECTION('ref_axis',(1.,0.,0.));
#4932=DIRECTION('',(-0.587785252292473,0.,0.809016994374947));
#4933=DIRECTION('center_axis',(0.,1.,0.));
#4934=DIRECTION('ref_axis',(1.,0.,0.));
#4935=DIRECTION('center_axis',(0.,-1.,0.));
#4936=DIRECTION('ref_axis',(0.309016994374947,0.,-0.951056516295154));
#4937=DIRECTION('center_axis',(0.,-1.,0.));
#4938=DIRECTION('ref_axis',(1.,0.,0.));
#4939=DIRECTION('',(-0.809016994374947,0.,0.587785252292473));
#4940=DIRECTION('center_axis',(0.,1.,0.));
#4941=DIRECTION('ref_axis',(1.,0.,0.));
#4942=DIRECTION('center_axis',(0.,-1.,0.));
#4943=DIRECTION('ref_axis',(0.309016994374947,0.,-0.951056516295154));
#4944=DIRECTION('center_axis',(0.,-1.,0.));
#4945=DIRECTION('ref_axis',(1.,0.,0.));
#4946=DIRECTION('',(-0.951056516295153,0.,0.309016994374948));
#4947=DIRECTION('center_axis',(0.,1.,0.));
#4948=DIRECTION('ref_axis',(1.,0.,0.));
#4949=DIRECTION('center_axis',(0.,-1.,0.));
#4950=DIRECTION('ref_axis',(0.309016994374947,0.,-0.951056516295154));
#4951=DIRECTION('center_axis',(0.,-1.,0.));
#4952=DIRECTION('ref_axis',(1.,0.,0.));
#4953=DIRECTION('',(0.309016994374948,0.,0.951056516295154));
#4954=DIRECTION('center_axis',(0.,1.,0.));
#4955=DIRECTION('ref_axis',(1.,0.,0.));
#4956=DIRECTION('center_axis',(-0.951056516295154,0.,-0.309016994374947));
#4957=DIRECTION('ref_axis',(0.309016994374947,0.,-0.951056516295154));
#4958=DIRECTION('',(0.,1.,0.));
#4959=DIRECTION('',(-0.309016994374947,0.,0.951056516295154));
#4960=DIRECTION('',(0.,-1.,0.));
#4961=DIRECTION('center_axis',(1.,0.,-1.66533453693773E-16));
#4962=DIRECTION('ref_axis',(1.66533453693773E-16,0.,1.));
#4963=DIRECTION('',(0.,1.,0.));
#4964=DIRECTION('',(-1.66533453693773E-16,0.,-1.));
#4965=DIRECTION('',(0.,-1.,0.));
#4966=DIRECTION('center_axis',(0.951056516295154,0.,0.309016994374947));
#4967=DIRECTION('ref_axis',(-0.309016994374947,0.,0.951056516295154));
#4968=DIRECTION('',(0.,1.,0.));
#4969=DIRECTION('',(0.309016994374947,0.,-0.951056516295154));
#4970=DIRECTION('',(0.,-1.,0.));
#4971=DIRECTION('center_axis',(-0.951056516295154,0.,0.309016994374948));
#4972=DIRECTION('ref_axis',(-0.309016994374948,0.,-0.951056516295154));
#4973=DIRECTION('',(0.,1.,0.));
#4974=DIRECTION('',(0.309016994374948,0.,0.951056516295154));
#4975=DIRECTION('',(0.,-1.,0.));
#4976=DIRECTION('center_axis',(0.951056516295154,0.,-0.309016994374948));
#4977=DIRECTION('ref_axis',(0.309016994374948,0.,0.951056516295154));
#4978=DIRECTION('',(0.,1.,0.));
#4979=DIRECTION('',(-0.309016994374948,0.,-0.951056516295154));
#4980=DIRECTION('',(0.,-1.,0.));
#4981=DIRECTION('center_axis',(0.809016994374947,0.,-0.587785252292473));
#4982=DIRECTION('ref_axis',(0.587785252292473,0.,0.809016994374947));
#4983=DIRECTION('',(0.,1.,0.));
#4984=DIRECTION('',(-0.587785252292473,0.,-0.809016994374947));
#4985=DIRECTION('',(0.,-1.,0.));
#4986=DIRECTION('center_axis',(-0.809016994374947,0.,0.587785252292473));
#4987=DIRECTION('ref_axis',(-0.587785252292473,0.,-0.809016994374947));
#4988=DIRECTION('',(0.,1.,0.));
#4989=DIRECTION('',(0.587785252292473,0.,0.809016994374947));
#4990=DIRECTION('',(0.,-1.,0.));
#4991=DIRECTION('center_axis',(-0.587785252292473,0.,0.809016994374947));
#4992=DIRECTION('ref_axis',(-0.809016994374947,0.,-0.587785252292473));
#4993=DIRECTION('',(0.,1.,0.));
#4994=DIRECTION('',(0.809016994374947,0.,0.587785252292473));
#4995=DIRECTION('',(0.,-1.,0.));
#4996=DIRECTION('center_axis',(0.587785252292473,0.,-0.809016994374947));
#4997=DIRECTION('ref_axis',(0.809016994374947,0.,0.587785252292473));
#4998=DIRECTION('',(0.,1.,0.));
#4999=DIRECTION('',(-0.809016994374947,0.,-0.587785252292473));
#5000=DIRECTION('',(0.,-1.,0.));
#5001=DIRECTION('center_axis',(0.309016994374947,0.,-0.951056516295154));
#5002=DIRECTION('ref_axis',(0.951056516295154,0.,0.309016994374947));
#5003=DIRECTION('',(0.,1.,0.));
#5004=DIRECTION('',(-0.951056516295154,0.,-0.309016994374947));
#5005=DIRECTION('',(0.,-1.,0.));
#5006=DIRECTION('center_axis',(-0.309016994374947,0.,0.951056516295154));
#5007=DIRECTION('ref_axis',(-0.951056516295154,0.,-0.309016994374947));
#5008=DIRECTION('',(0.,1.,0.));
#5009=DIRECTION('',(0.951056516295154,0.,0.309016994374947));
#5010=DIRECTION('',(0.,-1.,0.));
#5011=DIRECTION('center_axis',(5.55111512312578E-17,0.,1.));
#5012=DIRECTION('ref_axis',(-1.,0.,5.55111512312578E-17));
#5013=DIRECTION('',(0.,1.,0.));
#5014=DIRECTION('',(1.,0.,-5.55111512312578E-17));
#5015=DIRECTION('',(0.,-1.,0.));
#5016=DIRECTION('center_axis',(-1.11022302462516E-16,0.,-1.));
#5017=DIRECTION('ref_axis',(1.,0.,-1.11022302462516E-16));
#5018=DIRECTION('',(0.,1.,0.));
#5019=DIRECTION('',(-1.,0.,1.11022302462516E-16));
#5020=DIRECTION('',(0.,-1.,0.));
#5021=DIRECTION('center_axis',(-0.309016994374948,0.,-0.951056516295154));
#5022=DIRECTION('ref_axis',(0.951056516295154,0.,-0.309016994374948));
#5023=DIRECTION('',(0.,1.,0.));
#5024=DIRECTION('',(-0.951056516295154,0.,0.309016994374948));
#5025=DIRECTION('',(0.,-1.,0.));
#5026=DIRECTION('center_axis',(0.309016994374948,0.,0.951056516295154));
#5027=DIRECTION('ref_axis',(-0.951056516295154,0.,0.309016994374948));
#5028=DIRECTION('',(0.,1.,0.));
#5029=DIRECTION('',(0.951056516295154,0.,-0.309016994374948));
#5030=DIRECTION('',(0.,-1.,0.));
#5031=DIRECTION('center_axis',(0.587785252292473,0.,0.809016994374947));
#5032=DIRECTION('ref_axis',(-0.809016994374947,0.,0.587785252292473));
#5033=DIRECTION('',(0.,1.,0.));
#5034=DIRECTION('',(0.809016994374947,0.,-0.587785252292473));
#5035=DIRECTION('',(0.,-1.,0.));
#5036=DIRECTION('center_axis',(-0.587785252292473,0.,-0.809016994374947));
#5037=DIRECTION('ref_axis',(0.809016994374947,0.,-0.587785252292473));
#5038=DIRECTION('',(0.,1.,0.));
#5039=DIRECTION('',(-0.809016994374947,0.,0.587785252292473));
#5040=DIRECTION('',(0.,-1.,0.));
#5041=DIRECTION('center_axis',(0.809016994374948,0.,0.587785252292473));
#5042=DIRECTION('ref_axis',(-0.587785252292473,0.,0.809016994374947));
#5043=DIRECTION('',(0.,1.,0.));
#5044=DIRECTION('',(0.587785252292473,0.,-0.809016994374947));
#5045=DIRECTION('',(0.,-1.,0.));
#5046=DIRECTION('center_axis',(-0.809016994374948,0.,-0.587785252292473));
#5047=DIRECTION('ref_axis',(0.587785252292473,0.,-0.809016994374947));
#5048=DIRECTION('',(0.,1.,0.));
#5049=DIRECTION('',(-0.587785252292473,0.,0.809016994374947));
#5050=DIRECTION('',(0.,-1.,0.));
#5051=DIRECTION('center_axis',(0.,1.,0.));
#5052=DIRECTION('ref_axis',(1.,0.,0.));
#5053=DIRECTION('center_axis',(0.,-1.,0.));
#5054=DIRECTION('ref_axis',(1.,0.,0.));
#5055=DIRECTION('',(0.,-1.,0.));
#5056=DIRECTION('center_axis',(0.,-1.,0.));
#5057=DIRECTION('ref_axis',(1.,0.,0.));
#5058=DIRECTION('center_axis',(0.,-1.,0.));
#5059=DIRECTION('ref_axis',(1.,0.,0.));
#5060=DIRECTION('center_axis',(0.,-1.,0.));
#5061=DIRECTION('ref_axis',(1.,0.,0.));
#5062=DIRECTION('center_axis',(0.,-1.,0.));
#5063=DIRECTION('ref_axis',(1.,0.,0.));
#5064=DIRECTION('center_axis',(0.,-1.,0.));
#5065=DIRECTION('ref_axis',(1.,0.,0.));
#5066=DIRECTION('',(0.,1.,0.));
#5067=DIRECTION('center_axis',(0.,-1.,0.));
#5068=DIRECTION('ref_axis',(1.,0.,0.));
#5069=DIRECTION('',(0.,-1.,0.));
#5070=DIRECTION('center_axis',(0.,-1.,0.));
#5071=DIRECTION('ref_axis',(1.,0.,0.));
#5072=DIRECTION('center_axis',(0.,-1.,0.));
#5073=DIRECTION('ref_axis',(1.,0.,0.));
#5074=DIRECTION('center_axis',(0.,-1.,0.));
#5075=DIRECTION('ref_axis',(1.,0.,0.));
#5076=DIRECTION('center_axis',(0.,-1.,0.));
#5077=DIRECTION('ref_axis',(1.,0.,0.));
#5078=DIRECTION('center_axis',(0.,-1.,0.));
#5079=DIRECTION('ref_axis',(1.,0.,0.));
#5080=DIRECTION('center_axis',(0.,-1.,0.));
#5081=DIRECTION('ref_axis',(1.,0.,0.));
#5082=DIRECTION('center_axis',(0.,-1.,0.));
#5083=DIRECTION('ref_axis',(1.,0.,0.));
#5084=DIRECTION('center_axis',(0.,-1.,0.));
#5085=DIRECTION('ref_axis',(1.,0.,0.));
#5086=DIRECTION('center_axis',(0.,-1.,0.));
#5087=DIRECTION('ref_axis',(1.,0.,0.));
#5088=DIRECTION('center_axis',(0.,-1.,0.));
#5089=DIRECTION('ref_axis',(1.,0.,0.));
#5090=DIRECTION('center_axis',(0.,-1.,0.));
#5091=DIRECTION('ref_axis',(1.,0.,0.));
#5092=DIRECTION('center_axis',(0.,-1.,0.));
#5093=DIRECTION('ref_axis',(1.,0.,0.));
#5094=DIRECTION('center_axis',(0.,-1.,0.));
#5095=DIRECTION('ref_axis',(1.,0.,0.));
#5096=DIRECTION('center_axis',(0.,-1.,0.));
#5097=DIRECTION('ref_axis',(1.,0.,0.));
#5098=DIRECTION('center_axis',(0.,-1.,0.));
#5099=DIRECTION('ref_axis',(1.,0.,0.));
#5100=DIRECTION('center_axis',(0.,1.,0.));
#5101=DIRECTION('ref_axis',(1.,0.,0.));
#5102=DIRECTION('center_axis',(0.,1.,0.));
#5103=DIRECTION('ref_axis',(1.,0.,0.));
#5104=DIRECTION('',(5.02869919278543E-17,0.,1.));
#5105=DIRECTION('center_axis',(0.,1.,0.));
#5106=DIRECTION('ref_axis',(1.,0.,0.));
#5107=DIRECTION('center_axis',(0.,1.,0.));
#5108=DIRECTION('ref_axis',(1.,0.,0.));
#5109=DIRECTION('center_axis',(0.,1.,0.));
#5110=DIRECTION('ref_axis',(1.,0.,0.));
#5111=DIRECTION('center_axis',(0.,1.,0.));
#5112=DIRECTION('ref_axis',(1.,0.,0.));
#5113=DIRECTION('center_axis',(0.,1.,0.));
#5114=DIRECTION('ref_axis',(1.,0.,0.));
#5115=DIRECTION('center_axis',(0.,1.,0.));
#5116=DIRECTION('ref_axis',(1.,0.,0.));
#5117=DIRECTION('center_axis',(0.,1.,0.));
#5118=DIRECTION('ref_axis',(1.,0.,0.));
#5119=DIRECTION('center_axis',(0.,1.,0.));
#5120=DIRECTION('ref_axis',(1.,0.,0.));
#5121=DIRECTION('center_axis',(0.,1.,0.));
#5122=DIRECTION('ref_axis',(1.,0.,0.));
#5123=DIRECTION('center_axis',(0.,1.,0.));
#5124=DIRECTION('ref_axis',(1.,0.,0.));
#5125=DIRECTION('center_axis',(0.,1.,0.));
#5126=DIRECTION('ref_axis',(1.,0.,0.));
#5127=DIRECTION('',(0.,0.,-1.));
#5128=DIRECTION('center_axis',(0.,1.,0.));
#5129=DIRECTION('ref_axis',(1.,0.,0.));
#5130=DIRECTION('center_axis',(0.,1.,0.));
#5131=DIRECTION('ref_axis',(1.,0.,0.));
#5132=DIRECTION('center_axis',(0.,1.,0.));
#5133=DIRECTION('ref_axis',(1.,0.,0.));
#5134=DIRECTION('center_axis',(0.,1.,0.));
#5135=DIRECTION('ref_axis',(1.,0.,0.));
#5136=DIRECTION('center_axis',(0.,1.,0.));
#5137=DIRECTION('ref_axis',(1.,0.,0.));
#5138=DIRECTION('center_axis',(0.,1.,0.));
#5139=DIRECTION('ref_axis',(1.,0.,0.));
#5140=DIRECTION('center_axis',(0.,1.,0.));
#5141=DIRECTION('ref_axis',(1.,0.,0.));
#5142=DIRECTION('center_axis',(0.,1.,0.));
#5143=DIRECTION('ref_axis',(1.,0.,0.));
#5144=DIRECTION('center_axis',(0.,1.,0.));
#5145=DIRECTION('ref_axis',(1.,0.,0.));
#5146=DIRECTION('center_axis',(0.,1.,0.));
#5147=DIRECTION('ref_axis',(1.,0.,0.));
#5148=DIRECTION('center_axis',(0.,1.,0.));
#5149=DIRECTION('ref_axis',(1.,0.,0.));
#5150=DIRECTION('center_axis',(0.,1.,0.));
#5151=DIRECTION('ref_axis',(1.,0.,0.));
#5152=DIRECTION('center_axis',(0.,1.,0.));
#5153=DIRECTION('ref_axis',(1.,0.,0.));
#5154=DIRECTION('center_axis',(0.,1.,0.));
#5155=DIRECTION('ref_axis',(1.,0.,0.));
#5156=DIRECTION('center_axis',(0.,1.,0.));
#5157=DIRECTION('ref_axis',(1.,0.,0.));
#5158=DIRECTION('center_axis',(0.,1.,0.));
#5159=DIRECTION('ref_axis',(1.,0.,0.));
#5160=DIRECTION('center_axis',(0.,1.,0.));
#5161=DIRECTION('ref_axis',(1.,0.,0.));
#5162=DIRECTION('center_axis',(0.,1.,0.));
#5163=DIRECTION('ref_axis',(1.,0.,0.));
#5164=DIRECTION('center_axis',(0.,1.,0.));
#5165=DIRECTION('ref_axis',(1.,0.,0.));
#5166=DIRECTION('center_axis',(0.,1.,0.));
#5167=DIRECTION('ref_axis',(1.,0.,0.));
#5168=DIRECTION('center_axis',(0.,1.,0.));
#5169=DIRECTION('ref_axis',(1.,0.,0.));
#5170=DIRECTION('center_axis',(0.,1.,0.));
#5171=DIRECTION('ref_axis',(1.,0.,0.));
#5172=DIRECTION('center_axis',(0.,1.,0.));
#5173=DIRECTION('ref_axis',(1.,0.,0.));
#5174=DIRECTION('center_axis',(0.,1.,0.));
#5175=DIRECTION('ref_axis',(1.,0.,0.));
#5176=DIRECTION('center_axis',(0.,1.,0.));
#5177=DIRECTION('ref_axis',(1.,0.,0.));
#5178=DIRECTION('center_axis',(1.,0.,0.));
#5179=DIRECTION('ref_axis',(0.,0.,1.));
#5180=DIRECTION('',(0.,0.,1.));
#5181=DIRECTION('',(0.,1.,0.));
#5182=DIRECTION('center_axis',(0.,-1.,0.));
#5183=DIRECTION('ref_axis',(0.,0.,-1.));
#5184=DIRECTION('',(-5.02869919278543E-17,0.,-1.));
#5185=DIRECTION('center_axis',(0.,1.,0.));
#5186=DIRECTION('ref_axis',(1.,0.,0.));
#5187=DIRECTION('center_axis',(-1.,0.,5.02869919278543E-17));
#5188=DIRECTION('ref_axis',(-5.02869919278543E-17,0.,-1.));
#5189=DIRECTION('',(0.,-1.,0.));
#5190=DIRECTION('center_axis',(0.,1.,0.));
#5191=DIRECTION('ref_axis',(1.,0.,0.));
#5192=DIRECTION('center_axis',(0.,1.,0.));
#5193=DIRECTION('ref_axis',(1.,0.,0.));
#5194=DIRECTION('',(0.,-1.,0.));
#5195=DIRECTION('center_axis',(0.,1.,0.));
#5196=DIRECTION('ref_axis',(1.,0.,0.));
#5197=DIRECTION('center_axis',(0.,1.,0.));
#5198=DIRECTION('ref_axis',(1.,0.,0.));
#5199=DIRECTION('center_axis',(0.,1.,0.));
#5200=DIRECTION('ref_axis',(1.,0.,0.));
#5890=CARTESIAN_POINT('',(0.,0.,0.));
#5891=CARTESIAN_POINT('Origin',(-2.77555756156289E-16,0.75,150.));
#5892=CARTESIAN_POINT('',(-0.75,0.75,148.324135091683));
#5893=CARTESIAN_POINT('Ctrl Pts',(-0.75,0.75,148.324135091683));
#5894=CARTESIAN_POINT('Ctrl Pts',(-0.75,0.844174950069239,148.324135091683));
#5895=CARTESIAN_POINT('Ctrl Pts',(-0.731178490330683,0.944625017929177,
148.324566712535));
#5896=CARTESIAN_POINT('Ctrl Pts',(-0.654637296400931,1.12940860934839,148.326126918842));
#5897=CARTESIAN_POINT('Ctrl Pts',(-0.596917780711965,1.21374239106786,148.327233118533));
#5898=CARTESIAN_POINT('Ctrl Pts',(-0.463742391599736,1.34691778018009,148.329310633496));
#5899=CARTESIAN_POINT('Ctrl Pts',(-0.379408609590679,1.40463729616334,148.330416715758));
#5900=CARTESIAN_POINT('Ctrl Pts',(-0.194625017492537,1.48117849064877,148.331976653629));
#5901=CARTESIAN_POINT('Ctrl Pts',(-0.0941749493170033,1.5,148.33240815703));
#5902=CARTESIAN_POINT('Ctrl Pts',(0.0941749493170025,1.5,148.33240815703));
#5903=CARTESIAN_POINT('Ctrl Pts',(0.194625017492536,1.48117849064877,148.331976653629));
#5904=CARTESIAN_POINT('Ctrl Pts',(0.379408609590678,1.40463729616334,148.330416715758));
#5905=CARTESIAN_POINT('Ctrl Pts',(0.463742391599735,1.34691778018009,148.329310633496));
#5906=CARTESIAN_POINT('Ctrl Pts',(0.596917780711964,1.21374239106786,148.327233118533));
#5907=CARTESIAN_POINT('Ctrl Pts',(0.65463729640093,1.12940860934839,148.326126918842));
#5908=CARTESIAN_POINT('Ctrl Pts',(0.731178490330683,0.944625017929177,148.324566712535));
#5909=CARTESIAN_POINT('Ctrl Pts',(0.75,0.844174950069239,148.324135091683));
#5910=CARTESIAN_POINT('Ctrl Pts',(0.75,0.655825049930761,148.324135091683));
#5911=CARTESIAN_POINT('Ctrl Pts',(0.731178490330683,0.555374982070823,148.324566712535));
#5912=CARTESIAN_POINT('Ctrl Pts',(0.65463729640093,0.370591390651611,148.326126918842));
#5913=CARTESIAN_POINT('Ctrl Pts',(0.596917780711965,0.286257608932143,148.327233118533));
#5914=CARTESIAN_POINT('Ctrl Pts',(0.463742391599736,0.153082219819914,148.329310633496));
#5915=CARTESIAN_POINT('Ctrl Pts',(0.379408609590678,0.0953627038366558,
148.330416715758));
#5916=CARTESIAN_POINT('Ctrl Pts',(0.194625017492536,0.0188215093512261,
148.331976653629));
#5917=CARTESIAN_POINT('Ctrl Pts',(0.0941749493170028,-2.48722993596056E-16,
148.33240815703));
#5918=CARTESIAN_POINT('Ctrl Pts',(-0.0941749493170028,-3.06388518716522E-16,
148.33240815703));
#5919=CARTESIAN_POINT('Ctrl Pts',(-0.194625017492536,0.0188215093512259,
148.331976653629));
#5920=CARTESIAN_POINT('Ctrl Pts',(-0.379408609590678,0.0953627038366554,
148.330416715758));
#5921=CARTESIAN_POINT('Ctrl Pts',(-0.463742391599735,0.153082219819914,
148.329310633496));
#5922=CARTESIAN_POINT('Ctrl Pts',(-0.596917780711965,0.286257608932143,
148.327233118533));
#5923=CARTESIAN_POINT('Ctrl Pts',(-0.65463729640093,0.370591390651611,148.326126918842));
#5924=CARTESIAN_POINT('Ctrl Pts',(-0.731178490330683,0.555374982070822,
148.324566712535));
#5925=CARTESIAN_POINT('Ctrl Pts',(-0.75,0.655825049930761,148.324135091683));
#5926=CARTESIAN_POINT('Ctrl Pts',(-0.75,0.75,148.324135091683));
#5927=CARTESIAN_POINT('',(-0.75,0.75,143.));
#5928=CARTESIAN_POINT('',(-0.75,0.75,150.));
#5929=CARTESIAN_POINT('Origin',(-2.77555756156289E-16,0.75,143.));
#5930=CARTESIAN_POINT('Origin',(-2.77555756156289E-16,0.75,143.));
#5931=CARTESIAN_POINT('Origin',(21.3786362834003,0.,183.365153071209));
#5932=CARTESIAN_POINT('',(6.7681855290754,-0.5,138.398809313913));
#5933=CARTESIAN_POINT('',(6.76818552907538,-2.,138.398809313913));
#5934=CARTESIAN_POINT('',(6.76818552907538,-2.,138.398809313913));
#5935=CARTESIAN_POINT('',(9.55097594168496,-0.5,146.963357554211));
#5936=CARTESIAN_POINT('',(14.9826398548955,-0.5,163.680300159368));
#5937=CARTESIAN_POINT('',(9.55097594168495,-2.,146.963357554211));
#5938=CARTESIAN_POINT('',(9.55097594168495,-2.,146.963357554211));
#5939=CARTESIAN_POINT('',(10.2137898835526,-2.,149.003289111307));
#5940=CARTESIAN_POINT('Origin',(-10.3247007219358,0.,116.635644555059));
#5941=CARTESIAN_POINT('',(-24.0664011568829,-0.5,121.100593686106));
#5942=CARTESIAN_POINT('',(-24.0664011568829,-2.,121.100593686106));
#5943=CARTESIAN_POINT('',(-24.0664011568829,-2.,121.100593686106));
#5944=CARTESIAN_POINT('',(-32.6309493971805,-0.5,123.883384098715));
#5945=CARTESIAN_POINT('',(9.36015218990532,-0.5,110.239648126554));
#5946=CARTESIAN_POINT('',(-32.6309493971805,-2.,123.883384098715));
#5947=CARTESIAN_POINT('',(-32.6309493971805,-2.,123.883384098715));
#5948=CARTESIAN_POINT('',(-5.31685885815536,-2.,115.008498097897));
#5949=CARTESIAN_POINT('Origin',(-9.10763471134047,0.,119.713424126857));
#5950=CARTESIAN_POINT('',(-20.7970232944598,-0.5,128.206262058874));
#5951=CARTESIAN_POINT('',(-20.7970232944598,-2.,128.206262058874));
#5952=CARTESIAN_POINT('',(-20.7970232944598,-2.,128.206262058874));
#5953=CARTESIAN_POINT('',(-28.082463178239,-0.5,133.499443969666));
#5954=CARTESIAN_POINT('',(7.63730133040817,-0.5,107.547515963797));
#5955=CARTESIAN_POINT('',(-28.082463178239,-2.,133.499443969666));
#5956=CARTESIAN_POINT('',(-28.082463178239,-2.,133.499443969666));
#5957=CARTESIAN_POINT('',(-4.84770998181646,-2.,116.618407644756));
#5958=CARTESIAN_POINT('Origin',(-6.99904995857679,0.,122.264472363786));
#5959=CARTESIAN_POINT('',(-15.4918878905933,-0.5,133.953860946905));
#5960=CARTESIAN_POINT('',(-15.4918878905933,-2.,133.953860946905));
#5961=CARTESIAN_POINT('',(-15.4918878905933,-2.,133.953860946905));
#5962=CARTESIAN_POINT('',(-20.7850698013853,-0.5,141.239300830684));
#5963=CARTESIAN_POINT('',(5.16685820448335,-0.5,105.519536322037));
#5964=CARTESIAN_POINT('',(-20.7850698013853,-2.,141.239300830684));
#5965=CARTESIAN_POINT('',(-20.7850698013853,-2.,141.239300830684));
#5966=CARTESIAN_POINT('',(-3.90403347647587,-2.,118.004547634262));
#5967=CARTESIAN_POINT('Origin',(-4.20534943061909,0.,124.039074890216));
#5968=CARTESIAN_POINT('',(-8.6702985616657,-0.5,137.780775325163));
#5969=CARTESIAN_POINT('',(-8.6702985616657,-2.,137.780775325163));
#5970=CARTESIAN_POINT('',(-8.6702985616657,-2.,137.780775325163));
#5971=CARTESIAN_POINT('',(-11.4530889742753,-0.5,146.345323565461));
#5972=CARTESIAN_POINT('',(2.19064699788576,-0.5,104.354221978375));
#5973=CARTESIAN_POINT('',(-11.4530889742753,-2.,146.345323565461));
#5974=CARTESIAN_POINT('',(-11.4530889742753,-2.,146.345323565461));
#5975=CARTESIAN_POINT('',(-2.57820297345712,-2.,119.031233026436));
#5976=CARTESIAN_POINT('Origin',(-0.999999999999996,0.,186.592811973533));
#5977=CARTESIAN_POINT('',(-0.999999999999999,-0.5,139.312400150624));
#5978=CARTESIAN_POINT('',(-1.,-2.,139.312400150624));
#5979=CARTESIAN_POINT('',(-1.,-2.,139.312400150624));
#5980=CARTESIAN_POINT('',(-0.999999999999998,-0.5,148.317699092963));
#5981=CARTESIAN_POINT('',(-0.999999999999996,-0.5,165.894932747045));
#5982=CARTESIAN_POINT('',(-1.,-2.,148.317699092963));
#5983=CARTESIAN_POINT('',(-1.,-2.,148.317699092963));
#5984=CARTESIAN_POINT('',(-1.,-2.,150.462610065282));
#5985=CARTESIAN_POINT('Origin',(41.6645826936637,0.,173.380088117269));
#5986=CARTESIAN_POINT('',(13.8738539018434,-0.5,135.12943145149));
#5987=CARTESIAN_POINT('',(13.8738539018434,-2.,135.12943145149));
#5988=CARTESIAN_POINT('',(13.8738539018434,-2.,135.12943145149));
#5989=CARTESIAN_POINT('',(19.1670358126354,-0.5,142.414871335269));
#5990=CARTESIAN_POINT('',(29.4986745306036,-0.5,156.635152075521));
#5991=CARTESIAN_POINT('',(19.1670358126354,-2.,142.414871335269));
#5992=CARTESIAN_POINT('',(19.1670358126354,-2.,142.414871335269));
#5993=CARTESIAN_POINT('',(20.4277828496444,-2.,144.150140763296));
#5994=CARTESIAN_POINT('Origin',(57.872109455654,0.,157.615024839444));
#5995=CARTESIAN_POINT('',(19.6214527898748,-0.5,129.824296047624));
#5996=CARTESIAN_POINT('',(19.6214527898749,-2.,129.824296047624));
#5997=CARTESIAN_POINT('',(19.6214527898749,-2.,129.824296047624));
#5998=CARTESIAN_POINT('',(26.906892673654,-0.5,135.117477958416));
#5999=CARTESIAN_POINT('',(41.1271734139054,-0.5,145.449116676384));
#6000=CARTESIAN_POINT('',(26.906892673654,-2.,135.117477958416));
#6001=CARTESIAN_POINT('',(26.906892673654,-2.,135.117477958416));
#6002=CARTESIAN_POINT('',(28.6421621016808,-2.,136.378224995425));
#6003=CARTESIAN_POINT('Origin',(68.4147109254286,0.,137.613157473021));
#6004=CARTESIAN_POINT('',(23.448367168133,-0.5,123.002706718696));
#6005=CARTESIAN_POINT('',(23.448367168133,-2.,123.002706718696));
#6006=CARTESIAN_POINT('',(23.448367168133,-2.,123.002706718696));
#6007=CARTESIAN_POINT('',(32.0129154084306,-0.5,125.785497131306));
#6008=CARTESIAN_POINT('',(48.7298580135875,-0.5,131.217161044516));
#6009=CARTESIAN_POINT('',(32.0129154084306,-2.,125.785497131306));
#6010=CARTESIAN_POINT('',(32.0129154084306,-2.,125.785497131306));
#6011=CARTESIAN_POINT('',(34.0528469655268,-2.,126.448311073173));
#6012=CARTESIAN_POINT('Origin',(72.2604038165021,0.,115.33240815703));
#6013=CARTESIAN_POINT('',(24.9799919935936,-0.5,115.33240815703));
#6014=CARTESIAN_POINT('',(24.9799919935936,-2.,115.33240815703));
#6015=CARTESIAN_POINT('',(24.9799919935936,-2.,115.33240815703));
#6016=CARTESIAN_POINT('',(33.9852909359328,-0.5,115.33240815703));
#6017=CARTESIAN_POINT('',(51.5625245900145,-0.5,115.33240815703));
#6018=CARTESIAN_POINT('',(33.9852909359328,-2.,115.33240815703));
#6019=CARTESIAN_POINT('',(33.9852909359328,-2.,115.33240815703));
#6020=CARTESIAN_POINT('',(36.1302019082511,-2.,115.33240815703));
#6021=CARTESIAN_POINT('Origin',(69.0327449141785,0.,92.9537718736301));
#6022=CARTESIAN_POINT('',(24.0664011568829,-0.5,107.564222627955));
#6023=CARTESIAN_POINT('',(24.0664011568829,-2.,107.564222627955));
#6024=CARTESIAN_POINT('',(24.0664011568829,-2.,107.564222627955));
#6025=CARTESIAN_POINT('',(32.6309493971805,-0.5,104.781432215346));
#6026=CARTESIAN_POINT('',(49.3478920023374,-0.5,99.349768302135));
#6027=CARTESIAN_POINT('',(32.6309493971805,-2.,104.781432215346));
#6028=CARTESIAN_POINT('',(32.6309493971805,-2.,104.781432215346));
#6029=CARTESIAN_POINT('',(34.6708809542767,-2.,104.118618273478));
#6030=CARTESIAN_POINT('Origin',(59.047679960239,0.,72.6678254633667));
#6031=CARTESIAN_POINT('',(20.7970232944598,-0.5,100.458554255187));
#6032=CARTESIAN_POINT('',(20.7970232944598,-2.,100.458554255187));
#6033=CARTESIAN_POINT('',(20.7970232944598,-2.,100.458554255187));
#6034=CARTESIAN_POINT('',(28.082463178239,-0.5,95.165372344395));
#6035=CARTESIAN_POINT('',(42.3027439184904,-0.5,84.8337336264269));
#6036=CARTESIAN_POINT('',(28.082463178239,-2.,95.165372344395));
#6037=CARTESIAN_POINT('',(28.082463178239,-2.,95.165372344395));
#6038=CARTESIAN_POINT('',(29.8177326062657,-2.,93.9046253073861));
#6039=CARTESIAN_POINT('Origin',(43.2826166824136,0.,56.4602987013764));
#6040=CARTESIAN_POINT('',(15.4918878905933,-0.5,94.7109553671556));
#6041=CARTESIAN_POINT('',(15.4918878905933,-2.,94.7109553671556));
#6042=CARTESIAN_POINT('',(15.4918878905933,-2.,94.7109553671556));
#6043=CARTESIAN_POINT('',(20.7850698013853,-0.5,87.4255154833764));
#6044=CARTESIAN_POINT('',(31.1167085193535,-0.5,73.205234743125));
#6045=CARTESIAN_POINT('',(20.7850698013853,-2.,87.4255154833764));
#6046=CARTESIAN_POINT('',(20.7850698013853,-2.,87.4255154833764));
#6047=CARTESIAN_POINT('',(22.0458168383943,-2.,85.6902460553496));
#6048=CARTESIAN_POINT('Origin',(23.2807493159906,0.,45.9176972316019));
#6049=CARTESIAN_POINT('',(8.6702985616657,-0.5,90.8840409888974));
#6050=CARTESIAN_POINT('',(8.6702985616657,-2.,90.8840409888975));
#6051=CARTESIAN_POINT('',(8.6702985616657,-2.,90.8840409888975));
#6052=CARTESIAN_POINT('',(11.4530889742753,-0.5,82.3194927485999));
#6053=CARTESIAN_POINT('',(16.8847528874858,-0.5,65.602550143443));
#6054=CARTESIAN_POINT('',(11.4530889742753,-2.,82.3194927485999));
#6055=CARTESIAN_POINT('',(11.4530889742753,-2.,82.3194927485999));
#6056=CARTESIAN_POINT('',(12.1159029161429,-2.,80.2795611915036));
#6057=CARTESIAN_POINT('Origin',(-2.30323639802878,0.,104.007707435095));
#6058=CARTESIAN_POINT('',(-6.76818552907538,-0.5,90.2660070001475));
#6059=CARTESIAN_POINT('',(-6.76818552907539,-2.,90.2660070001475));
#6060=CARTESIAN_POINT('',(-6.76818552907539,-2.,90.2660070001475));
#6061=CARTESIAN_POINT('',(-9.55097594168494,-0.5,81.70145875985));
#6062=CARTESIAN_POINT('',(4.09276003047609,-0.5,123.692560346936));
#6063=CARTESIAN_POINT('',(-9.55097594168495,-2.,81.70145875985));
#6064=CARTESIAN_POINT('',(-9.55097594168495,-2.,81.70145875985));
#6065=CARTESIAN_POINT('',(-0.67608994086681,-2.,109.015549298875));
#6066=CARTESIAN_POINT('Origin',(-5.38101596982691,0.,105.22477344569));
#6067=CARTESIAN_POINT('',(-13.8738539018434,-0.5,93.5353848625706));
#6068=CARTESIAN_POINT('',(-13.8738539018435,-2.,93.5353848625707));
#6069=CARTESIAN_POINT('',(-13.8738539018435,-2.,93.5353848625707));
#6070=CARTESIAN_POINT('',(-19.1670358126355,-0.5,86.2499449787914));
#6071=CARTESIAN_POINT('',(6.78489219323324,-0.5,121.969709487439));
#6072=CARTESIAN_POINT('',(-19.1670358126355,-2.,86.2499449787915));
#6073=CARTESIAN_POINT('',(-19.1670358126355,-2.,86.2499449787915));
#6074=CARTESIAN_POINT('',(-2.285999487726,-2.,109.484698175214));
#6075=CARTESIAN_POINT('Origin',(-7.93206420675555,0.,107.333358198454));
#6076=CARTESIAN_POINT('',(-19.6214527898749,-0.5,98.8405202664372));
#6077=CARTESIAN_POINT('',(-19.6214527898749,-2.,98.8405202664371));
#6078=CARTESIAN_POINT('',(-19.6214527898749,-2.,98.8405202664371));
#6079=CARTESIAN_POINT('',(-26.9068926736541,-0.5,93.5473383556452));
#6080=CARTESIAN_POINT('',(8.81287183499309,-0.5,119.499266361514));
#6081=CARTESIAN_POINT('',(-26.9068926736541,-2.,93.5473383556451));
#6082=CARTESIAN_POINT('',(-26.9068926736541,-2.,93.5473383556451));
#6083=CARTESIAN_POINT('',(-3.67213947723154,-2.,110.428374680555));
#6084=CARTESIAN_POINT('Origin',(-9.70666673318587,0.,110.127058726411));
#6085=CARTESIAN_POINT('',(-23.448367168133,-0.5,105.662109595365));
#6086=CARTESIAN_POINT('',(-23.448367168133,-2.,105.662109595365));
#6087=CARTESIAN_POINT('',(-23.448367168133,-2.,105.662109595365));
#6088=CARTESIAN_POINT('',(-32.0129154084306,-0.5,102.879319182755));
#6089=CARTESIAN_POINT('',(9.97818617865523,-0.5,116.523055154916));
#6090=CARTESIAN_POINT('',(-32.0129154084306,-2.,102.879319182755));
#6091=CARTESIAN_POINT('',(-32.0129154084306,-2.,102.879319182755));
#6092=CARTESIAN_POINT('',(-4.69882486940547,-2.,111.754205183573));
#6093=CARTESIAN_POINT('Origin',(-10.5311130894481,0.,113.33240815703));
#6094=CARTESIAN_POINT('',(-24.9799919935936,-0.5,113.33240815703));
#6095=CARTESIAN_POINT('',(-24.9799919935936,-2.,113.33240815703));
#6096=CARTESIAN_POINT('',(-24.9799919935936,-2.,113.33240815703));
#6097=CARTESIAN_POINT('',(-33.9852909359328,-0.5,113.33240815703));
#6098=CARTESIAN_POINT('',(10.1667661370394,-0.5,113.33240815703));
#6099=CARTESIAN_POINT('',(-33.9852909359328,-2.,113.33240815703));
#6100=CARTESIAN_POINT('',(-33.9852909359328,-2.,113.33240815703));
#6101=CARTESIAN_POINT('',(-5.26555654472407,-2.,113.33240815703));
#6102=CARTESIAN_POINT('Origin',(9.53769994268576,-0.5,84.9783860609091));
#6103=CARTESIAN_POINT('',(-24.9799919935936,-0.5,115.33240815703));
#6104=CARTESIAN_POINT('',(-25.,-0.5,114.33240815703));
#6105=CARTESIAN_POINT('Origin',(-2.22044604925031E-15,-0.5,114.33240815703));
#6106=CARTESIAN_POINT('',(-33.9852909359328,-0.5,115.33240815703));
#6107=CARTESIAN_POINT('',(-10.1667661370394,-0.5,115.33240815703));
#6108=CARTESIAN_POINT('',(-34.,-0.5,114.33240815703));
#6109=CARTESIAN_POINT('Origin',(-2.22044604925031E-15,-0.5,114.33240815703));
#6110=CARTESIAN_POINT('Origin',(-2.22044604925031E-15,-0.5,114.33240815703));
#6111=CARTESIAN_POINT('Origin',(-2.22044604925031E-15,-0.5,114.33240815703));
#6112=CARTESIAN_POINT('Origin',(9.53769994268576,-0.5,84.9783860609091));
#6113=CARTESIAN_POINT('',(-24.0664011568829,-0.5,107.564222627955));
#6114=CARTESIAN_POINT('Origin',(-2.22044604925031E-15,-0.5,114.33240815703));
#6115=CARTESIAN_POINT('',(-32.6309493971805,-0.5,104.781432215346));
#6116=CARTESIAN_POINT('',(-9.97818617865522,-0.5,112.141761159145));
#6117=CARTESIAN_POINT('Origin',(-2.22044604925031E-15,-0.5,114.33240815703));
#6118=CARTESIAN_POINT('Origin',(9.53769994268576,-0.5,84.9783860609091));
#6119=CARTESIAN_POINT('',(-20.7970232944598,-0.5,100.458554255187));
#6120=CARTESIAN_POINT('Origin',(-2.22044604925031E-15,-0.5,114.33240815703));
#6121=CARTESIAN_POINT('',(-28.082463178239,-0.5,95.165372344395));
#6122=CARTESIAN_POINT('',(-8.81287183499312,-0.5,109.165549952547));
#6123=CARTESIAN_POINT('Origin',(-2.22044604925031E-15,-0.5,114.33240815703));
#6124=CARTESIAN_POINT('Origin',(9.53769994268576,-0.5,84.9783860609091));
#6125=CARTESIAN_POINT('',(-15.4918878905933,-0.5,94.7109553671556));
#6126=CARTESIAN_POINT('Origin',(-2.22044604925031E-15,-0.5,114.33240815703));
#6127=CARTESIAN_POINT('',(-20.7850698013853,-0.5,87.4255154833764));
#6128=CARTESIAN_POINT('',(-6.78489219323324,-0.5,106.695106826622));
#6129=CARTESIAN_POINT('Origin',(-2.22044604925031E-15,-0.5,114.33240815703));
#6130=CARTESIAN_POINT('Origin',(9.53769994268576,-0.5,84.9783860609091));
#6131=CARTESIAN_POINT('',(-8.67029856166571,-0.5,90.8840409888974));
#6132=CARTESIAN_POINT('Origin',(-2.22044604925031E-15,-0.5,114.33240815703));
#6133=CARTESIAN_POINT('',(-11.4530889742753,-0.5,82.3194927485999));
#6134=CARTESIAN_POINT('',(-4.09276003047608,-0.5,104.972255967125));
#6135=CARTESIAN_POINT('Origin',(-2.22044604925031E-15,-0.5,114.33240815703));
#6136=CARTESIAN_POINT('Origin',(9.53769994268576,-0.5,84.9783860609091));
#6137=CARTESIAN_POINT('',(6.76818552907538,-0.5,90.2660070001475));
#6138=CARTESIAN_POINT('Origin',(-2.22044604925031E-15,-0.5,114.33240815703));
#6139=CARTESIAN_POINT('',(9.55097594168495,-0.5,81.70145875985));
#6140=CARTESIAN_POINT('',(2.19064699788576,-0.5,104.354221978375));
#6141=CARTESIAN_POINT('Origin',(-2.22044604925031E-15,-0.5,114.33240815703));
#6142=CARTESIAN_POINT('Origin',(9.53769994268576,-0.5,84.9783860609091));
#6143=CARTESIAN_POINT('',(13.8738539018434,-0.5,93.5353848625706));
#6144=CARTESIAN_POINT('Origin',(-2.22044604925031E-15,-0.5,114.33240815703));
#6145=CARTESIAN_POINT('',(19.1670358126354,-0.5,86.2499449787914));
#6146=CARTESIAN_POINT('',(5.16685820448335,-0.5,105.519536322037));
#6147=CARTESIAN_POINT('Origin',(-2.22044604925031E-15,-0.5,114.33240815703));
#6148=CARTESIAN_POINT('Origin',(9.53769994268576,-0.5,84.9783860609091));
#6149=CARTESIAN_POINT('',(19.6214527898749,-0.5,98.8405202664372));
#6150=CARTESIAN_POINT('Origin',(-2.22044604925031E-15,-0.5,114.33240815703));
#6151=CARTESIAN_POINT('',(26.9068926736541,-0.5,93.5473383556452));
#6152=CARTESIAN_POINT('',(7.63730133040817,-0.5,107.547515963797));
#6153=CARTESIAN_POINT('Origin',(-2.22044604925031E-15,-0.5,114.33240815703));
#6154=CARTESIAN_POINT('Origin',(9.53769994268576,-0.5,84.9783860609091));
#6155=CARTESIAN_POINT('',(23.448367168133,-0.5,105.662109595365));
#6156=CARTESIAN_POINT('Origin',(-2.22044604925031E-15,-0.5,114.33240815703));
#6157=CARTESIAN_POINT('',(32.0129154084306,-0.5,102.879319182755));
#6158=CARTESIAN_POINT('',(9.36015218990532,-0.5,110.239648126554));
#6159=CARTESIAN_POINT('Origin',(-2.22044604925031E-15,-0.5,114.33240815703));
#6160=CARTESIAN_POINT('Origin',(9.53769994268576,-0.5,84.9783860609091));
#6161=CARTESIAN_POINT('',(24.9799919935936,-0.5,113.33240815703));
#6162=CARTESIAN_POINT('Origin',(-2.22044604925031E-15,-0.5,114.33240815703));
#6163=CARTESIAN_POINT('',(33.9852909359328,-0.5,113.33240815703));
#6164=CARTESIAN_POINT('',(10.1667661370394,-0.5,113.33240815703));
#6165=CARTESIAN_POINT('Origin',(-2.22044604925031E-15,-0.5,114.33240815703));
#6166=CARTESIAN_POINT('Origin',(9.53769994268576,-0.5,84.9783860609091));
#6167=CARTESIAN_POINT('',(24.0664011568829,-0.5,121.100593686106));
#6168=CARTESIAN_POINT('Origin',(-2.22044604925031E-15,-0.5,114.33240815703));
#6169=CARTESIAN_POINT('',(32.6309493971805,-0.5,123.883384098715));
#6170=CARTESIAN_POINT('',(9.97818617865523,-0.5,116.523055154916));
#6171=CARTESIAN_POINT('Origin',(-2.22044604925031E-15,-0.5,114.33240815703));
#6172=CARTESIAN_POINT('Origin',(9.53769994268576,-0.5,84.9783860609091));
#6173=CARTESIAN_POINT('',(20.7970232944598,-0.5,128.206262058874));
#6174=CARTESIAN_POINT('Origin',(-2.22044604925031E-15,-0.5,114.33240815703));
#6175=CARTESIAN_POINT('',(28.082463178239,-0.5,133.499443969666));
#6176=CARTESIAN_POINT('',(8.81287183499309,-0.5,119.499266361514));
#6177=CARTESIAN_POINT('Origin',(-2.22044604925031E-15,-0.5,114.33240815703));
#6178=CARTESIAN_POINT('Origin',(9.53769994268576,-0.5,84.9783860609091));
#6179=CARTESIAN_POINT('',(15.4918878905933,-0.5,133.953860946905));
#6180=CARTESIAN_POINT('Origin',(-2.22044604925031E-15,-0.5,114.33240815703));
#6181=CARTESIAN_POINT('',(20.7850698013853,-0.5,141.239300830684));
#6182=CARTESIAN_POINT('',(6.78489219323324,-0.5,121.969709487439));
#6183=CARTESIAN_POINT('Origin',(-2.22044604925031E-15,-0.5,114.33240815703));
#6184=CARTESIAN_POINT('Origin',(9.53769994268576,-0.5,84.9783860609091));
#6185=CARTESIAN_POINT('',(1.,-0.5,139.312400150624));
#6186=CARTESIAN_POINT('Origin',(-2.22044604925031E-15,-0.5,114.33240815703));
#6187=CARTESIAN_POINT('',(1.,-0.5,148.317699092963));
#6188=CARTESIAN_POINT('',(1.,-0.5,124.49917429407));
#6189=CARTESIAN_POINT('Origin',(-2.22044604925031E-15,-0.5,114.33240815703));
#6190=CARTESIAN_POINT('Origin',(9.53769994268576,-0.5,84.9783860609091));
#6191=CARTESIAN_POINT('',(-6.76818552907539,-0.5,138.398809313913));
#6192=CARTESIAN_POINT('Origin',(-2.22044604925031E-15,-0.5,114.33240815703));
#6193=CARTESIAN_POINT('',(-9.55097594168495,-0.5,146.963357554211));
#6194=CARTESIAN_POINT('',(-2.19064699788578,-0.5,124.310594335686));
#6195=CARTESIAN_POINT('Origin',(-2.22044604925031E-15,-0.5,114.33240815703));
#6196=CARTESIAN_POINT('Origin',(9.53769994268576,-0.5,84.9783860609091));
#6197=CARTESIAN_POINT('',(-13.8738539018434,-0.5,135.12943145149));
#6198=CARTESIAN_POINT('Origin',(-2.22044604925031E-15,-0.5,114.33240815703));
#6199=CARTESIAN_POINT('',(-19.1670358126354,-0.5,142.414871335269));
#6200=CARTESIAN_POINT('',(-5.16685820448335,-0.5,123.145279992024));
#6201=CARTESIAN_POINT('Origin',(-2.22044604925031E-15,-0.5,114.33240815703));
#6202=CARTESIAN_POINT('Origin',(9.53769994268576,-0.5,84.9783860609091));
#6203=CARTESIAN_POINT('',(-19.6214527898749,-0.5,129.824296047624));
#6204=CARTESIAN_POINT('Origin',(-2.22044604925031E-15,-0.5,114.33240815703));
#6205=CARTESIAN_POINT('',(-26.906892673654,-0.5,135.117477958416));
#6206=CARTESIAN_POINT('',(-7.63730133040816,-0.5,121.117300350264));
#6207=CARTESIAN_POINT('Origin',(-2.22044604925031E-15,-0.5,114.33240815703));
#6208=CARTESIAN_POINT('Origin',(9.53769994268576,-0.5,84.9783860609091));
#6209=CARTESIAN_POINT('',(-23.448367168133,-0.5,123.002706718696));
#6210=CARTESIAN_POINT('Origin',(-2.22044604925031E-15,-0.5,114.33240815703));
#6211=CARTESIAN_POINT('',(-32.0129154084306,-0.5,125.785497131306));
#6212=CARTESIAN_POINT('',(-9.36015218990532,-0.5,118.425168187507));
#6213=CARTESIAN_POINT('Origin',(-2.22044604925031E-15,-0.5,114.33240815703));
#6214=CARTESIAN_POINT('Origin',(9.53769994268576,-0.5,84.9783860609091));
#6215=CARTESIAN_POINT('',(8.67029856166571,-0.5,137.780775325163));
#6216=CARTESIAN_POINT('Origin',(-2.22044604925031E-15,-0.5,114.33240815703));
#6217=CARTESIAN_POINT('',(11.4530889742753,-0.5,146.345323565461));
#6218=CARTESIAN_POINT('',(4.09276003047609,-0.5,123.692560346936));
#6219=CARTESIAN_POINT('Origin',(-2.22044604925031E-15,-0.5,114.33240815703));
#6220=CARTESIAN_POINT('Origin',(-4.20534943061909,0.,124.039074890216));
#6221=CARTESIAN_POINT('',(6.76818552907538,-2.,90.2660070001475));
#6222=CARTESIAN_POINT('',(6.76818552907538,-2.,90.2660070001475));
#6223=CARTESIAN_POINT('',(9.55097594168495,-2.,81.70145875985));
#6224=CARTESIAN_POINT('',(-2.57820297345712,-2.,119.031233026436));
#6225=CARTESIAN_POINT('',(9.55097594168495,-2.,81.70145875985));
#6226=CARTESIAN_POINT('Origin',(0.999999999999996,0.,103.801295067582));
#6227=CARTESIAN_POINT('',(1.,-2.,139.312400150624));
#6228=CARTESIAN_POINT('',(1.,-2.,139.312400150624));
#6229=CARTESIAN_POINT('',(1.,-2.,148.317699092963));
#6230=CARTESIAN_POINT('',(0.999999999999998,-2.,109.066851612306));
#6231=CARTESIAN_POINT('',(1.,-2.,148.317699092963));
#6232=CARTESIAN_POINT('Origin',(23.2807493159906,0.,45.9176972316019));
#6233=CARTESIAN_POINT('',(-6.76818552907539,-2.,138.398809313913));
#6234=CARTESIAN_POINT('',(-6.76818552907539,-2.,138.398809313913));
#6235=CARTESIAN_POINT('',(-9.55097594168495,-2.,146.963357554211));
#6236=CARTESIAN_POINT('',(12.1159029161429,-2.,80.2795611915036));
#6237=CARTESIAN_POINT('',(-9.55097594168495,-2.,146.963357554211));
#6238=CARTESIAN_POINT('Origin',(21.3786362834003,0.,183.365153071209));
#6239=CARTESIAN_POINT('',(-8.67029856166571,-2.,90.8840409888974));
#6240=CARTESIAN_POINT('',(-8.67029856166571,-2.,90.8840409888974));
#6241=CARTESIAN_POINT('',(-11.4530889742753,-2.,82.3194927485999));
#6242=CARTESIAN_POINT('',(10.2137898835526,-2.,149.003289111307));
#6243=CARTESIAN_POINT('',(-11.4530889742753,-2.,82.3194927485999));
#6244=CARTESIAN_POINT('Origin',(-2.30323639802878,0.,104.007707435095));
#6245=CARTESIAN_POINT('',(8.6702985616657,-2.,137.780775325163));
#6246=CARTESIAN_POINT('',(8.6702985616657,-2.,137.780775325163));
#6247=CARTESIAN_POINT('',(11.4530889742753,-2.,146.345323565461));
#6248=CARTESIAN_POINT('',(-0.67608994086681,-2.,109.015549298875));
#6249=CARTESIAN_POINT('',(11.4530889742753,-2.,146.345323565461));
#6250=CARTESIAN_POINT('Origin',(-5.38101596982691,0.,105.22477344569));
#6251=CARTESIAN_POINT('',(15.4918878905933,-2.,133.953860946905));
#6252=CARTESIAN_POINT('',(15.4918878905933,-2.,133.953860946905));
#6253=CARTESIAN_POINT('',(20.7850698013853,-2.,141.239300830684));
#6254=CARTESIAN_POINT('',(-2.285999487726,-2.,109.484698175214));
#6255=CARTESIAN_POINT('',(20.7850698013853,-2.,141.239300830684));
#6256=CARTESIAN_POINT('Origin',(41.6645826936637,0.,173.380088117269));
#6257=CARTESIAN_POINT('',(-15.4918878905934,-2.,94.7109553671556));
#6258=CARTESIAN_POINT('',(-15.4918878905934,-2.,94.7109553671556));
#6259=CARTESIAN_POINT('',(-20.7850698013854,-2.,87.4255154833764));
#6260=CARTESIAN_POINT('',(20.4277828496444,-2.,144.150140763296));
#6261=CARTESIAN_POINT('',(-20.7850698013854,-2.,87.4255154833764));
#6262=CARTESIAN_POINT('Origin',(57.872109455654,0.,157.615024839444));
#6263=CARTESIAN_POINT('',(-20.7970232944598,-2.,100.458554255187));
#6264=CARTESIAN_POINT('',(-20.7970232944598,-2.,100.458554255187));
#6265=CARTESIAN_POINT('',(-28.082463178239,-2.,95.165372344395));
#6266=CARTESIAN_POINT('',(28.6421621016808,-2.,136.378224995425));
#6267=CARTESIAN_POINT('',(-28.082463178239,-2.,95.165372344395));
#6268=CARTESIAN_POINT('Origin',(-7.93206420675555,0.,107.333358198454));
#6269=CARTESIAN_POINT('',(20.7970232944598,-2.,128.206262058874));
#6270=CARTESIAN_POINT('',(20.7970232944598,-2.,128.206262058874));
#6271=CARTESIAN_POINT('',(28.082463178239,-2.,133.499443969666));
#6272=CARTESIAN_POINT('',(-3.67213947723154,-2.,110.428374680555));
#6273=CARTESIAN_POINT('',(28.082463178239,-2.,133.499443969666));
#6274=CARTESIAN_POINT('Origin',(-9.70666673318587,0.,110.127058726411));
#6275=CARTESIAN_POINT('',(24.0664011568829,-2.,121.100593686106));
#6276=CARTESIAN_POINT('',(24.0664011568829,-2.,121.100593686106));
#6277=CARTESIAN_POINT('',(32.6309493971805,-2.,123.883384098715));
#6278=CARTESIAN_POINT('',(-4.69882486940547,-2.,111.754205183573));
#6279=CARTESIAN_POINT('',(32.6309493971805,-2.,123.883384098715));
#6280=CARTESIAN_POINT('Origin',(68.4147109254286,0.,137.613157473021));
#6281=CARTESIAN_POINT('',(-24.0664011568829,-2.,107.564222627955));
#6282=CARTESIAN_POINT('',(-24.0664011568829,-2.,107.564222627955));
#6283=CARTESIAN_POINT('',(-32.6309493971805,-2.,104.781432215346));
#6284=CARTESIAN_POINT('',(34.0528469655268,-2.,126.448311073173));
#6285=CARTESIAN_POINT('',(-32.6309493971805,-2.,104.781432215346));
#6286=CARTESIAN_POINT('Origin',(72.2604038165021,0.,115.33240815703));
#6287=CARTESIAN_POINT('',(-24.9799919935936,-2.,115.33240815703));
#6288=CARTESIAN_POINT('',(-24.9799919935936,-2.,115.33240815703));
#6289=CARTESIAN_POINT('',(-33.9852909359328,-2.,115.33240815703));
#6290=CARTESIAN_POINT('',(36.1302019082511,-2.,115.33240815703));
#6291=CARTESIAN_POINT('',(-33.9852909359328,-2.,115.33240815703));
#6292=CARTESIAN_POINT('Origin',(-10.5311130894481,0.,113.33240815703));
#6293=CARTESIAN_POINT('',(24.9799919935936,-2.,113.33240815703));
#6294=CARTESIAN_POINT('',(24.9799919935936,-2.,113.33240815703));
#6295=CARTESIAN_POINT('',(33.9852909359328,-2.,113.33240815703));
#6296=CARTESIAN_POINT('',(-5.26555654472407,-2.,113.33240815703));
#6297=CARTESIAN_POINT('',(33.9852909359328,-2.,113.33240815703));
#6298=CARTESIAN_POINT('Origin',(-10.3247007219358,0.,116.635644555059));
#6299=CARTESIAN_POINT('',(23.448367168133,-2.,105.662109595365));
#6300=CARTESIAN_POINT('',(23.448367168133,-2.,105.662109595365));
#6301=CARTESIAN_POINT('',(32.0129154084306,-2.,102.879319182755));
#6302=CARTESIAN_POINT('',(-5.31685885815536,-2.,115.008498097897));
#6303=CARTESIAN_POINT('',(32.0129154084306,-2.,102.879319182755));
#6304=CARTESIAN_POINT('Origin',(69.0327449141785,0.,92.9537718736301));
#6305=CARTESIAN_POINT('',(-23.448367168133,-2.,123.002706718696));
#6306=CARTESIAN_POINT('',(-23.448367168133,-2.,123.002706718696));
#6307=CARTESIAN_POINT('',(-32.0129154084306,-2.,125.785497131306));
#6308=CARTESIAN_POINT('',(34.6708809542767,-2.,104.118618273478));
#6309=CARTESIAN_POINT('',(-32.0129154084306,-2.,125.785497131306));
#6310=CARTESIAN_POINT('Origin',(59.047679960239,0.,72.6678254633667));
#6311=CARTESIAN_POINT('',(-19.6214527898749,-2.,129.824296047624));
#6312=CARTESIAN_POINT('',(-19.6214527898749,-2.,129.824296047624));
#6313=CARTESIAN_POINT('',(-26.906892673654,-2.,135.117477958416));
#6314=CARTESIAN_POINT('',(29.8177326062657,-2.,93.9046253073861));
#6315=CARTESIAN_POINT('',(-26.906892673654,-2.,135.117477958416));
#6316=CARTESIAN_POINT('Origin',(-9.10763471134047,0.,119.713424126857));
#6317=CARTESIAN_POINT('',(19.6214527898749,-2.,98.8405202664371));
#6318=CARTESIAN_POINT('',(19.6214527898749,-2.,98.8405202664371));
#6319=CARTESIAN_POINT('',(26.9068926736541,-2.,93.5473383556451));
#6320=CARTESIAN_POINT('',(-4.84770998181646,-2.,116.618407644756));
#6321=CARTESIAN_POINT('',(26.9068926736541,-2.,93.5473383556451));
#6322=CARTESIAN_POINT('Origin',(43.2826166824136,0.,56.4602987013764));
#6323=CARTESIAN_POINT('',(-13.8738539018434,-2.,135.12943145149));
#6324=CARTESIAN_POINT('',(-13.8738539018434,-2.,135.12943145149));
#6325=CARTESIAN_POINT('',(-19.1670358126354,-2.,142.414871335269));
#6326=CARTESIAN_POINT('',(22.0458168383943,-2.,85.6902460553496));
#6327=CARTESIAN_POINT('',(-19.1670358126354,-2.,142.414871335269));
#6328=CARTESIAN_POINT('Origin',(-6.99904995857679,0.,122.264472363786));
#6329=CARTESIAN_POINT('',(13.8738539018434,-2.,93.5353848625706));
#6330=CARTESIAN_POINT('',(13.8738539018434,-2.,93.5353848625706));
#6331=CARTESIAN_POINT('',(19.1670358126354,-2.,86.2499449787914));
#6332=CARTESIAN_POINT('',(-3.90403347647587,-2.,118.004547634262));
#6333=CARTESIAN_POINT('',(19.1670358126354,-2.,86.2499449787914));
#6334=CARTESIAN_POINT('Origin',(-2.22044604925031E-15,-2.,114.33240815703));
#6335=CARTESIAN_POINT('',(-25.,2.,114.33240815703));
#6336=CARTESIAN_POINT('Origin',(-2.22044604925031E-15,2.,114.33240815703));
#6337=CARTESIAN_POINT('',(-25.,-2.,114.33240815703));
#6338=CARTESIAN_POINT('Origin',(-2.22044604925031E-15,-2.,114.33240815703));
#6339=CARTESIAN_POINT('Origin',(-2.22044604925031E-15,-2.,114.33240815703));
#6340=CARTESIAN_POINT('Origin',(-2.22044604925031E-15,-2.,114.33240815703));
#6341=CARTESIAN_POINT('Origin',(-2.22044604925031E-15,-2.,114.33240815703));
#6342=CARTESIAN_POINT('',(-1.,-2.,89.3524161634369));
#6343=CARTESIAN_POINT('Origin',(-2.22044604925031E-15,-2.,114.33240815703));
#6344=CARTESIAN_POINT('',(-1.,-0.5,89.3524161634369));
#6345=CARTESIAN_POINT('',(-1.,-2.,89.3524161634369));
#6346=CARTESIAN_POINT('',(1.,-0.5,89.3524161634369));
#6347=CARTESIAN_POINT('Origin',(-2.22044604925031E-15,-0.5,114.33240815703));
#6348=CARTESIAN_POINT('',(1.,-2.,89.3524161634369));
#6349=CARTESIAN_POINT('',(1.,-2.,89.3524161634369));
#6350=CARTESIAN_POINT('Origin',(-2.22044604925031E-15,-2.,114.33240815703));
#6351=CARTESIAN_POINT('Origin',(-2.22044604925031E-15,-2.,114.33240815703));
#6352=CARTESIAN_POINT('Origin',(-2.22044604925031E-15,-2.,114.33240815703));
#6353=CARTESIAN_POINT('Origin',(-2.22044604925031E-15,-2.,114.33240815703));
#6354=CARTESIAN_POINT('Origin',(-2.22044604925031E-15,-2.,114.33240815703));
#6355=CARTESIAN_POINT('Origin',(-2.22044604925031E-15,-2.,114.33240815703));
#6356=CARTESIAN_POINT('Origin',(-2.22044604925031E-15,-2.,114.33240815703));
#6357=CARTESIAN_POINT('Origin',(-2.22044604925031E-15,-2.,114.33240815703));
#6358=CARTESIAN_POINT('Origin',(-2.22044604925031E-15,-2.,114.33240815703));
#6359=CARTESIAN_POINT('Origin',(-2.22044604925031E-15,-2.,114.33240815703));
#6360=CARTESIAN_POINT('Origin',(-2.22044604925031E-15,-2.,114.33240815703));
#6361=CARTESIAN_POINT('Origin',(-2.22044604925031E-15,-2.,114.33240815703));
#6362=CARTESIAN_POINT('Origin',(-2.22044604925031E-15,-2.,114.33240815703));
#6363=CARTESIAN_POINT('Origin',(-2.22044604925031E-15,-2.,114.33240815703));
#6364=CARTESIAN_POINT('Origin',(-2.22044604925031E-15,-2.,114.33240815703));
#6365=CARTESIAN_POINT('Origin',(0.,-2.,114.33240815703));
#6366=CARTESIAN_POINT('',(-1.,-2.,80.3471172210976));
#6367=CARTESIAN_POINT('Origin',(-2.22044604925031E-15,-2.,114.33240815703));
#6368=CARTESIAN_POINT('',(-1.,-2.,119.597964701755));
#6369=CARTESIAN_POINT('Origin',(0.,-2.,114.33240815703));
#6370=CARTESIAN_POINT('Origin',(-2.22044604925031E-15,-2.,114.33240815703));
#6371=CARTESIAN_POINT('Origin',(0.,-2.,114.33240815703));
#6372=CARTESIAN_POINT('Origin',(-2.22044604925031E-15,-2.,114.33240815703));
#6373=CARTESIAN_POINT('Origin',(0.,-2.,114.33240815703));
#6374=CARTESIAN_POINT('Origin',(-2.22044604925031E-15,-2.,114.33240815703));
#6375=CARTESIAN_POINT('Origin',(0.,-2.,114.33240815703));
#6376=CARTESIAN_POINT('Origin',(-2.22044604925031E-15,-2.,114.33240815703));
#6377=CARTESIAN_POINT('Origin',(0.,-2.,114.33240815703));
#6378=CARTESIAN_POINT('Origin',(-2.22044604925031E-15,-2.,114.33240815703));
#6379=CARTESIAN_POINT('Origin',(0.,-2.,114.33240815703));
#6380=CARTESIAN_POINT('',(1.,-2.,80.3471172210976));
#6381=CARTESIAN_POINT('',(1.,-2.,78.2022062487794));
#6382=CARTESIAN_POINT('Origin',(-2.22044604925031E-15,-2.,114.33240815703));
#6383=CARTESIAN_POINT('Origin',(0.,-2.,114.33240815703));
#6384=CARTESIAN_POINT('Origin',(-2.22044604925031E-15,-2.,114.33240815703));
#6385=CARTESIAN_POINT('Origin',(0.,-2.,114.33240815703));
#6386=CARTESIAN_POINT('Origin',(-2.22044604925031E-15,-2.,114.33240815703));
#6387=CARTESIAN_POINT('Origin',(0.,-2.,114.33240815703));
#6388=CARTESIAN_POINT('Origin',(-2.22044604925031E-15,-2.,114.33240815703));
#6389=CARTESIAN_POINT('Origin',(0.,-2.,114.33240815703));
#6390=CARTESIAN_POINT('Origin',(-2.22044604925031E-15,-2.,114.33240815703));
#6391=CARTESIAN_POINT('Origin',(0.,-2.,114.33240815703));
#6392=CARTESIAN_POINT('Origin',(-2.22044604925031E-15,-2.,114.33240815703));
#6393=CARTESIAN_POINT('Origin',(0.,-2.,114.33240815703));
#6394=CARTESIAN_POINT('Origin',(-2.22044604925031E-15,-2.,114.33240815703));
#6395=CARTESIAN_POINT('Origin',(0.,-2.,114.33240815703));
#6396=CARTESIAN_POINT('Origin',(-2.22044604925031E-15,-2.,114.33240815703));
#6397=CARTESIAN_POINT('Origin',(0.,-2.,114.33240815703));
#6398=CARTESIAN_POINT('Origin',(-2.22044604925031E-15,-2.,114.33240815703));
#6399=CARTESIAN_POINT('Origin',(0.,-2.,114.33240815703));
#6400=CARTESIAN_POINT('Origin',(-2.22044604925031E-15,-2.,114.33240815703));
#6401=CARTESIAN_POINT('Origin',(0.,-2.,114.33240815703));
#6402=CARTESIAN_POINT('Origin',(-2.22044604925031E-15,-2.,114.33240815703));
#6403=CARTESIAN_POINT('Origin',(0.,-2.,114.33240815703));
#6404=CARTESIAN_POINT('Origin',(-2.22044604925031E-15,-2.,114.33240815703));
#6405=CARTESIAN_POINT('Origin',(0.,-2.,114.33240815703));
#6406=CARTESIAN_POINT('Origin',(-2.22044604925031E-15,-2.,114.33240815703));
#6407=CARTESIAN_POINT('Origin',(1.,0.,42.0720043405283));
#6408=CARTESIAN_POINT('',(1.,-0.5,80.3471172210976));
#6409=CARTESIAN_POINT('',(1.,-0.5,62.7698835670159));
#6410=CARTESIAN_POINT('',(1.,-2.,80.3471172210976));
#6411=CARTESIAN_POINT('Origin',(-2.08166817117217E-15,-0.5,83.4677627935035));
#6412=CARTESIAN_POINT('',(-1.,-0.5,80.3471172210976));
#6413=CARTESIAN_POINT('',(-1.,-0.5,104.165642019991));
#6414=CARTESIAN_POINT('Origin',(-2.22044604925031E-15,-0.5,114.33240815703));
#6415=CARTESIAN_POINT('Origin',(-1.,0.,124.863521246479));
#6416=CARTESIAN_POINT('',(-1.,-2.,80.3471172210976));
#6417=CARTESIAN_POINT('Origin',(-2.22044604925031E-15,-2.,114.33240815703));
#6418=CARTESIAN_POINT('',(-34.,2.,114.33240815703));
#6419=CARTESIAN_POINT('Origin',(-2.22044604925031E-15,2.,114.33240815703));
#6420=CARTESIAN_POINT('',(-34.,-2.,114.33240815703));
#6421=CARTESIAN_POINT('Origin',(-2.22044604925031E-15,-2.,114.33240815703));
#6422=CARTESIAN_POINT('Origin',(0.,2.,114.33240815703));
#6423=CARTESIAN_POINT('Origin',(0.,-2.,114.33240815703));
#6730=UNCERTAINTY_MEASURE_WITH_UNIT(LENGTH_MEASURE(0.01),#6754,
'DISTANCE_ACCURACY_VALUE',
'Maximum model space distance between geometric entities at asserted c
onnectivities');
#6738=UNCERTAINTY_MEASURE_WITH_UNIT(LENGTH_MEASURE(0.01),#6754,
'DISTANCE_ACCURACY_VALUE',
'Maximum model space distance between geometric entities at asserted c
onnectivities');
#6745=(
GEOMETRIC_REPRESENTATION_CONTEXT(3)
GLOBAL_UNCERTAINTY_ASSIGNED_CONTEXT((#6730))
GLOBAL_UNIT_ASSIGNED_CONTEXT((#6754,#6756,#6757))
REPRESENTATION_CONTEXT('','3D')
);
#6753=(
GEOMETRIC_REPRESENTATION_CONTEXT(3)
GLOBAL_UNCERTAINTY_ASSIGNED_CONTEXT((#6738))
GLOBAL_UNIT_ASSIGNED_CONTEXT((#6754,#6756,#6757))
REPRESENTATION_CONTEXT('','3D')
);
#6754=(
LENGTH_UNIT()
NAMED_UNIT(*)
SI_UNIT(.MILLI.,.METRE.)
);
#6756=(
NAMED_UNIT(*)
PLANE_ANGLE_UNIT()
SI_UNIT($,.RADIAN.)
);
#6757=(
NAMED_UNIT(*)
SI_UNIT($,.STERADIAN.)
SOLID_ANGLE_UNIT()
);
#6764=SHAPE_DEFINITION_REPRESENTATION(#6778,#6805);
#6778=PRODUCT_DEFINITION_SHAPE('',$,#6820);
#6805=SHAPE_REPRESENTATION('',(#4048),#6745);
#6813=PRODUCT_DEFINITION_CONTEXT('part definition',#6857,'design');
#6820=PRODUCT_DEFINITION('Disc','Disc',#6834,#6813);
#6834=PRODUCT_DEFINITION_FORMATION('',$,#6865);
#6857=APPLICATION_CONTEXT(
'Core Data for Automotive Mechanical Design Process');
#6858=PRODUCT_CONTEXT('part definition',#6857,'mechanical');
#6865=PRODUCT('Disc','Disc',$,(#6858));
#6901=COLOUR_RGB('Light Blue',0.38,0.62,0.78);
#6902=FILL_AREA_STYLE_COLOUR('',#6901);
#6903=FILL_AREA_STYLE('',(#6902));
#6904=SURFACE_STYLE_FILL_AREA(#6903);
#6905=SURFACE_SIDE_STYLE('',(#6904));
#6906=SURFACE_STYLE_USAGE(.BOTH.,#6905);
#6907=PRESENTATION_STYLE_ASSIGNMENT((#6906));
ENDSEC;
END-ISO-10303-21;
